ISO-10303-21;
HEADER;
FILE_DESCRIPTION (('STEP AP214'),
    '1' );
FILE_NAME ('MirrorHeavy Cast Iron Table Bed Base.step',
    '2026-10-21T17:07:05',
    ( '' ),
    ( '' ),
    'SwSTEP 2.0',
    'SolidWorks 2025',
    '' );
FILE_SCHEMA (( 'AUTOMOTIVE_DESIGN' ));
ENDSEC;

DATA;
#39=LINE ( 'NONE', #14132, #32055 ) ;
#78=EDGE_CURVE ( 'NONE', #4330, #41889, #5365, .T. ) ;
#149=LINE ( 'NONE', #21398, #31138 ) ;
#164=VECTOR ( 'NONE', #10534, 1000.000000000000000 ) ;
#184=EDGE_CURVE ( 'NONE', #12197, #1931, #19516, .T. ) ;
#234=DIRECTION ( 'NONE',  ( 1.000000000000000000, 0.000000000000000000, 0.000000000000000000 ) ) ;
#242=CIRCLE ( 'NONE', #11326, 24.99999999999991118 ) ;
#288=CARTESIAN_POINT ( 'NONE',  ( 919.9999999999993179, 219.9999999999998863, -360.0000000000000000 ) ) ;
#328=CARTESIAN_POINT ( 'NONE',  ( 914.9999999999992042, 74.99999999999984368, 360.0000000000000000 ) ) ;
#382=MECHANICAL_DESIGN_GEOMETRIC_PRESENTATION_REPRESENTATION('',(#11425),#4082);
#452=CARTESIAN_POINT ( 'NONE',  ( -2.220446049250310809E-13, 479.9999999999994884, 0.000000000000000000 ) ) ;
#454=VECTOR ( 'NONE', #45378, 1000.000000000000114 ) ;
#497=DIRECTION ( 'NONE',  ( 0.000000000000000000, 0.000000000000000000, -1.000000000000000000 ) ) ;
#544=CARTESIAN_POINT ( 'NONE',  ( 914.9999999999992042, 56.60618624968562074, -350.0000000000000000 ) ) ;
#548=DIRECTION ( 'NONE',  ( 0.000000000000000000, 0.000000000000000000, -1.000000000000000000 ) ) ;
#560=CARTESIAN_POINT ( 'NONE',  ( 989.9999999999992042, 469.9999999999999432, 350.0000000000000000 ) ) ;
#577=VERTEX_POINT ( 'NONE', #10432 ) ;
#607=CARTESIAN_POINT ( 'NONE',  ( 919.9999999999993179, 219.9999999999998863, -360.0000000000000000 ) ) ;
#711=EDGE_CURVE ( 'NONE', #43956, #10766, #14370, .T. ) ;
#726=CARTESIAN_POINT ( 'NONE',  ( 999.9999999999992042, 239.9999999999998863, -360.0000000000000000 ) ) ;
#795=CARTESIAN_POINT ( 'NONE',  ( 999.9999999999992042, 249.9999999999998863, -360.0000000000000000 ) ) ;
#965=LINE ( 'NONE', #21311, #37445 ) ;
#982=CARTESIAN_POINT ( 'NONE',  ( 999.5857864376259840, -600.0000000000001137, 360.0000000000000000 ) ) ;
#992=ADVANCED_FACE ( 'NONE', ( #19750 ), #19977, .F. ) ;
#1001=VECTOR ( 'NONE', #11333, 1000.000000000000000 ) ;
#1007=ORIENTED_EDGE ( 'NONE', *, *, #29695, .T. ) ;
#1036=ORIENTED_EDGE ( 'NONE', *, *, #41383, .F. ) ;
#1044=CARTESIAN_POINT ( 'NONE',  ( 989.9999999999992042, -590.0000000000001137, 209.9999999999999716 ) ) ;
#1048=DIRECTION ( 'NONE',  ( -0.000000000000000000, -0.000000000000000000, 1.000000000000000000 ) ) ;
#1155=VERTEX_POINT ( 'NONE', #15822 ) ;
#1164=ORIENTED_EDGE ( 'NONE', *, *, #21005, .T. ) ;
#1202=( LENGTH_UNIT ( ) NAMED_UNIT ( * ) SI_UNIT ( .MILLI., .METRE. ) );
#1247=LINE ( 'NONE', #26404, #9266 ) ;
#1277=VERTEX_POINT ( 'NONE', #26450 ) ;
#1279=CARTESIAN_POINT ( 'NONE',  ( 919.9999999999993179, 219.9999999999998863, -360.0000000000000000 ) ) ;
#1367=ORIENTED_EDGE ( 'NONE', *, *, #16471, .T. ) ;
#1423=ORIENTED_EDGE ( 'NONE', *, *, #13394, .F. ) ;
#1444=CARTESIAN_POINT ( 'NONE',  ( 939.9999999999993179, -419.8175818341089780, 209.9999999999999716 ) ) ;
#1462=FACE_OUTER_BOUND ( 'NONE', #18383, .T. ) ;
#1498=CARTESIAN_POINT ( 'NONE',  ( 989.9999999999992042, -414.5899773927342835, 209.9999999999999716 ) ) ;
#1539=ADVANCED_FACE ( 'NONE', ( #27820 ), #3100, .T. ) ;
#1594=AXIS2_PLACEMENT_3D ( 'NONE', #10655, #18050, #497 ) ;
#1664=CARTESIAN_POINT ( 'NONE',  ( 989.9999999999992042, 62.85347435602256638, -357.4246812887967053 ) ) ;
#1670=CARTESIAN_POINT ( 'NONE',  ( 989.9999999999992042, 50.81038600091411439, 217.3872392842761769 ) ) ;
#1677=DIRECTION ( 'NONE',  ( -0.000000000000000000, -0.000000000000000000, 1.000000000000000000 ) ) ;
#1688=DIRECTION ( 'NONE',  ( 1.000000000000000000, 0.000000000000000000, 0.000000000000000000 ) ) ;
#1691=VERTEX_POINT ( 'NONE', #560 ) ;
#1697=CARTESIAN_POINT ( 'NONE',  ( 999.5857864376259840, 249.9999999999998863, -360.0000000000000000 ) ) ;
#1698=CYLINDRICAL_SURFACE ( 'NONE', #43242, 24.99999999999991118 ) ;
#1801=AXIS2_PLACEMENT_3D ( 'NONE', #17086, #35085, #42250 ) ;
#1803=ORIENTED_EDGE ( 'NONE', *, *, #30300, .T. ) ;
#1806=AXIS2_PLACEMENT_3D ( 'NONE', #7030, #17662, #3576 ) ;
#1819=DIRECTION ( 'NONE',  ( -2.750100768424433062E-32, 1.672022627447525240E-16, -1.000000000000000000 ) ) ;
#1844=CARTESIAN_POINT ( 'NONE',  ( 879.9999999999992042, 99.99999999999984368, -350.0000000000000000 ) ) ;
#1854=AXIS2_PLACEMENT_3D ( 'NONE', #40565, #2202, #36645 ) ;
#1884=ORIENTED_EDGE ( 'NONE', *, *, #10316, .T. ) ;
#1908=LINE ( 'NONE', #16016, #40236 ) ;
#1914=AXIS2_PLACEMENT_3D ( 'NONE', #1279, #25296, #17927 ) ;
#1924=ORIENTED_EDGE ( 'NONE', *, *, #9522, .F. ) ;
#1931=VERTEX_POINT ( 'NONE', #26828 ) ;
#1940=DIRECTION ( 'NONE',  ( 0.000000000000000000, 0.000000000000000000, -1.000000000000000000 ) ) ;
#1981=ORIENTED_EDGE ( 'NONE', *, *, #5195, .T. ) ;
#2042=ORIENTED_EDGE ( 'NONE', *, *, #43308, .F. ) ;
#2080=DIRECTION ( 'NONE',  ( 1.000000000000000000, 0.000000000000000000, 0.000000000000000000 ) ) ;
#2130=DIRECTION ( 'NONE',  ( -0.000000000000000000, -0.6438296778008192334, 0.7651688349527135946 ) ) ;
#2147=ORIENTED_EDGE ( 'NONE', *, *, #33217, .T. ) ;
#2202=DIRECTION ( 'NONE',  ( 0.000000000000000000, 0.000000000000000000, -1.000000000000000000 ) ) ;
#2210=LINE ( 'NONE', #33395, #10574 ) ;
#2224=CARTESIAN_POINT ( 'NONE',  ( 879.9999999999992042, 249.9999999999998295, 199.9999999999999716 ) ) ;
#2283=ORIENTED_EDGE ( 'NONE', *, *, #14859, .F. ) ;
#2337=ORIENTED_EDGE ( 'NONE', *, *, #26661, .T. ) ;
#2348=EDGE_CURVE ( 'NONE', #15471, #14853, #35138, .T. ) ;
#2354=ADVANCED_FACE ( 'NONE', ( #17137 ), #31220, .T. ) ;
#2366=EDGE_CURVE ( 'NONE', #13298, #42174, #13677, .T. ) ;
#2385=ADVANCED_FACE ( 'NONE', ( #10426 ), #27305, .T. ) ;
#2404=CARTESIAN_POINT ( 'NONE',  ( 999.5857864376259840, 249.9999999999998863, 199.9999999999999432 ) ) ;
#2411=EDGE_CURVE ( 'NONE', #29177, #25389, #27757, .T. ) ;
#2421=EDGE_CURVE ( 'NONE', #28819, #1277, #39, .T. ) ;
#2515=ORIENTED_EDGE ( 'NONE', *, *, #33217, .F. ) ;
#2551=PLANE ( 'NONE',  #31550 ) ;
#2639=CARTESIAN_POINT ( 'NONE',  ( 939.9999999999993179, -600.0000000000001137, -360.0000000000000000 ) ) ;
#2643=CARTESIAN_POINT ( 'NONE',  ( 998.9999999999992042, 249.9999999999998863, 199.9999999999999716 ) ) ;
#2659=CYLINDRICAL_SURFACE ( 'NONE', #27621, 1.000000000000000888 ) ;
#2713=CARTESIAN_POINT ( 'NONE',  ( 914.9999999999992042, 74.99999999999984368, -360.0000000000000000 ) ) ;
#2789=VERTEX_POINT ( 'NONE', #27025 ) ;
#2810=CARTESIAN_POINT ( 'NONE',  ( 187.1337867209877857, -185.0721577059061644, -75.19946970736494052 ) ) ;
#2862=MANIFOLD_SOLID_BREP ( '<Heavy Cast Iron Table Bed Base>-<Fillet2>', #27633 ) ;
#2867=ORIENTED_EDGE ( 'NONE', *, *, #33082, .T. ) ;
#2870=DIRECTION ( 'NONE',  ( 0.000000000000000000, -1.000000000000000000, -1.672022627447524993E-16 ) ) ;
#2927=CARTESIAN_POINT ( 'NONE',  ( 879.9999999999992042, 99.99999999999984368, -350.0000000000000000 ) ) ;
#2933=LINE ( 'NONE', #19798, #13472 ) ;
#2982=DIRECTION ( 'NONE',  ( 0.000000000000000000, -0.6594541114781790059, -0.7517448203044204691 ) ) ;
#3022=ORIENTED_EDGE ( 'NONE', *, *, #32275, .F. ) ;
#3030=VERTEX_POINT ( 'NONE', #3217 ) ;
#3054=VECTOR ( 'NONE', #29626, 1000.000000000000000 ) ;
#3077=ORIENTED_EDGE ( 'NONE', *, *, #33082, .F. ) ;
#3091=CARTESIAN_POINT ( 'NONE',  ( 989.9999999999992042, 240.0000000000001990, 201.9999999999999716 ) ) ;
#3095=DIRECTION ( 'NONE',  ( 0.000000000000000000, -0.6594541114781790059, -0.7517448203044204691 ) ) ;
#3097=LINE ( 'NONE', #10720, #15942 ) ;
#3100=CYLINDRICAL_SURFACE ( 'NONE', #33467, 1.000000000000000888 ) ;
#3107=CARTESIAN_POINT ( 'NONE',  ( 939.9999999999993179, -590.0000000000001137, -360.0000000000000000 ) ) ;
#3113=FACE_OUTER_BOUND ( 'NONE', #38208, .T. ) ;
#3130=ADVANCED_FACE ( 'NONE', ( #27469 ), #31625, .F. ) ;
#3162=PLANE ( 'NONE',  #5755 ) ;
#3164=ORIENTED_EDGE ( 'NONE', *, *, #27411, .F. ) ;
#3177=PRODUCT_DEFINITION_FORMATION_WITH_SPECIFIED_SOURCE ( 'ANY', '', #6326, .NOT_KNOWN. ) ;
#3217=CARTESIAN_POINT ( 'NONE',  ( 939.9999999999992042, 46.15097736693707020, -350.0000000000000000 ) ) ;
#3230=EDGE_CURVE ( 'NONE', #20750, #15194, #21736, .T. ) ;
#3268=EDGE_CURVE ( 'NONE', #5854, #2789, #37873, .T. ) ;
#3276=DIRECTION ( 'NONE',  ( -0.000000000000000000, -0.000000000000000000, -1.000000000000000000 ) ) ;
#3316=EDGE_CURVE ( 'NONE', #28329, #4120, #38339, .T. ) ;
#3415=VERTEX_POINT ( 'NONE', #14308 ) ;
#3482=PLANE ( 'NONE',  #17576 ) ;
#3506=ADVANCED_FACE ( 'NONE', ( #35777 ), #24919, .F. ) ;
#3576=DIRECTION ( 'NONE',  ( -1.000000000000000000, 0.000000000000000000, 0.000000000000000000 ) ) ;
#3592=DIRECTION ( 'NONE',  ( 0.000000000000000000, 0.000000000000000000, -1.000000000000000000 ) ) ;
#3597=EDGE_CURVE ( 'NONE', #2789, #10930, #41580, .T. ) ;
#3603=VERTEX_POINT ( 'NONE', #12710 ) ;
#3610=PRODUCT_DEFINITION ( 'UNKNOWN', '', #3177, #12551 ) ;
#3624=DIRECTION ( 'NONE',  ( -0.000000000000000000, -0.6438296778008192334, 0.7651688349527135946 ) ) ;
#3625=PLANE ( 'NONE',  #4125 ) ;
#3655=ORIENTED_EDGE ( 'NONE', *, *, #27411, .T. ) ;
#3671=LINE ( 'NONE', #30417, #17960 ) ;
#3686=DIRECTION ( 'NONE',  ( 1.000000000000000000, 4.625929269271485914E-16, 0.000000000000000000 ) ) ;
#3711=ORIENTED_EDGE ( 'NONE', *, *, #37418, .F. ) ;
#3733=PLANE ( 'NONE',  #1594 ) ;
#3739=CARTESIAN_POINT ( 'NONE',  ( 914.9999999999992042, 99.99999999999984368, -360.0000000000000000 ) ) ;
#3783=PLANE ( 'NONE',  #13583 ) ;
#3832=CARTESIAN_POINT ( 'NONE',  ( 939.9999999999993179, -590.0000000000001137, 209.9999999999999716 ) ) ;
#3852=CARTESIAN_POINT ( 'NONE',  ( 914.9999999999992042, 99.99999999999984368, -360.0000000000000000 ) ) ;
#3859=CARTESIAN_POINT ( 'NONE',  ( 914.9999999999992042, 99.99999999999984368, 360.0000000000000000 ) ) ;
#3866=DIRECTION ( 'NONE',  ( 0.000000000000000000, 0.000000000000000000, -1.000000000000000000 ) ) ;
#4001=DIRECTION ( 'NONE',  ( 0.000000000000000000, 0.7651688349527167032, 0.6438296778008156807 ) ) ;
#4064=ADVANCED_FACE ( 'NONE', ( #14287 ), #39469, .F. ) ;
#4078=DIRECTION ( 'NONE',  ( 0.000000000000000000, 1.000000000000000000, 0.000000000000000000 ) ) ;
#4080=VECTOR ( 'NONE', #42549, 1000.000000000000000 ) ;
#4082=( GEOMETRIC_REPRESENTATION_CONTEXT ( 3 ) GLOBAL_UNCERTAINTY_ASSIGNED_CONTEXT ( ( #12105 ) ) GLOBAL_UNIT_ASSIGNED_CONTEXT ( ( #12261, #26559, #8797 ) ) REPRESENTATION_CONTEXT ( 'NONE', 'WORKASPACE' ) );
#4103=ORIENTED_EDGE ( 'NONE', *, *, #34208, .T. ) ;
#4120=VERTEX_POINT ( 'NONE', #22332 ) ;
#4125=AXIS2_PLACEMENT_3D ( 'NONE', #17713, #10773, #13327 ) ;
#4154=CARTESIAN_POINT ( 'NONE',  ( 919.9999999999993179, 219.9999999999998863, -360.0000000000000000 ) ) ;
#4170=ORIENTED_EDGE ( 'NONE', *, *, #42160, .F. ) ;
#4176=CARTESIAN_POINT ( 'NONE',  ( 919.9999999999993179, 219.9999999999998863, -359.9749999999999659 ) ) ;
#4177=DIRECTION ( 'NONE',  ( -1.058954862565134068E-16, 0.6438296778008191223, -0.7651688349527137056 ) ) ;
#4187=VECTOR ( 'NONE', #5345, 1000.000000000000000 ) ;
#4204=DIRECTION ( 'NONE',  ( -0.000000000000000000, -0.000000000000000000, 1.000000000000000000 ) ) ;
#4208=DIRECTION ( 'NONE',  ( -0.000000000000000000, -0.000000000000000000, 1.000000000000000000 ) ) ;
#4223=VECTOR ( 'NONE', #36106, 1000.000000000000000 ) ;
#4254=ORIENTED_EDGE ( 'NONE', *, *, #42215, .F. ) ;
#4285=ORIENTED_EDGE ( 'NONE', *, *, #33494, .F. ) ;
#4292=ORIENTED_EDGE ( 'NONE', *, *, #2348, .F. ) ;
#4298=CARTESIAN_POINT ( 'NONE',  ( 999.9999999999992042, 239.9999999999998863, -350.0000000000000000 ) ) ;
#4330=VERTEX_POINT ( 'NONE', #12790 ) ;
#4380=PLANE ( 'NONE',  #16549 ) ;
#4383=LINE ( 'NONE', #23199, #26921 ) ;
#4391=AXIS2_PLACEMENT_3D ( 'NONE', #36742, #36069, #5101 ) ;
#4392=ORIENTED_EDGE ( 'NONE', *, *, #41885, .F. ) ;
#4434=CARTESIAN_POINT ( 'NONE',  ( 879.9999999999990905, 479.9999999999998863, 360.0000000000000000 ) ) ;
#4468=DIRECTION ( 'NONE',  ( 0.000000000000000000, -1.000000000000000000, 0.000000000000000000 ) ) ;
#4479=DIRECTION ( 'NONE',  ( 0.000000000000000000, 0.000000000000000000, -1.000000000000000000 ) ) ;
#4518=ORIENTED_EDGE ( 'NONE', *, *, #32275, .T. ) ;
#4551=CARTESIAN_POINT ( 'NONE',  ( 914.9999999999992042, 74.99999999999984368, 350.0000000000000000 ) ) ;
#4661=CIRCLE ( 'NONE', #30461, 7.999999999999785061 ) ;
#4676=ORIENTED_EDGE ( 'NONE', *, *, #36243, .T. ) ;
#4686=ORIENTED_EDGE ( 'NONE', *, *, #26628, .F. ) ;
#4708=CIRCLE ( 'NONE', #30512, 8.000000000000007105 ) ;
#4763=VECTOR ( 'NONE', #3276, 1000.000000000000000 ) ;
#4825=ORIENTED_EDGE ( 'NONE', *, *, #26674, .F. ) ;
#4827=AXIS2_PLACEMENT_3D ( 'NONE', #39235, #28358, #14976 ) ;
#4893=EDGE_LOOP ( 'NONE', ( #22004, #21958, #27948, #5004 ) ) ;
#4895=ORIENTED_EDGE ( 'NONE', *, *, #17095, .T. ) ;
#4896=( NAMED_UNIT ( * ) PLANE_ANGLE_UNIT ( ) SI_UNIT ( $, .RADIAN. ) );
#4913=CARTESIAN_POINT ( 'NONE',  ( 911.9999999999993179, 154.9999999999998863, 350.0000000000000000 ) ) ;
#4919=CARTESIAN_POINT ( 'NONE',  ( 989.9999999999992042, 249.9999999999998863, -350.0000000000000000 ) ) ;
#4941=CARTESIAN_POINT ( 'NONE',  ( 939.9999999999993179, 62.79977829742944095, 207.3621835540873235 ) ) ;
#4951=DIRECTION ( 'NONE',  ( 0.000000000000000000, 1.000000000000000000, 0.000000000000000000 ) ) ;
#5004=ORIENTED_EDGE ( 'NONE', *, *, #26661, .F. ) ;
#5047=ORIENTED_EDGE ( 'NONE', *, *, #16809, .T. ) ;
#5101=DIRECTION ( 'NONE',  ( 0.000000000000000000, 0.000000000000000000, 1.000000000000000000 ) ) ;
#5133=CARTESIAN_POINT ( 'NONE',  ( 989.9999999999992042, 62.79977829742938411, 207.3621835540872951 ) ) ;
#5145=EDGE_CURVE ( 'NONE', #21201, #6854, #40028, .T. ) ;
#5161=CARTESIAN_POINT ( 'NONE',  ( 939.9999999999993179, -600.0000000000001137, -360.0000000000000000 ) ) ;
#5169=VERTEX_POINT ( 'NONE', #4913 ) ;
#5195=EDGE_CURVE ( 'NONE', #5495, #22719, #39348, .T. ) ;
#5210=EDGE_CURVE ( 'NONE', #11422, #28329, #14873, .T. ) ;
#5293=CARTESIAN_POINT ( 'NONE',  ( 879.9999999999992042, 99.99999999999984368, -360.0000000000000000 ) ) ;
#5294=CARTESIAN_POINT ( 'NONE',  ( 939.9999999999994316, -428.4497686941065240, -352.6378164459125628 ) ) ;
#5310=LINE ( 'NONE', #22864, #23241 ) ;
#5341=ORIENTED_EDGE ( 'NONE', *, *, #32907, .T. ) ;
#5345=DIRECTION ( 'NONE',  ( 0.000000000000000000, -0.6594541114781790059, -0.7517448203044204691 ) ) ;
#5365=LINE ( 'NONE', #29865, #9928 ) ;
#5394=DIRECTION ( 'NONE',  ( -1.000000000000000000, -4.625929269271485914E-16, -0.000000000000000000 ) ) ;
#5448=VERTEX_POINT ( 'NONE', #41165 ) ;
#5462=CARTESIAN_POINT ( 'NONE',  ( 939.9999999999992042, 240.0000000000000568, 210.0000000000000000 ) ) ;
#5485=CARTESIAN_POINT ( 'NONE',  ( 939.9999999999993179, -600.0000000000001137, 350.0000000000000000 ) ) ;
#5490=EDGE_CURVE ( 'NONE', #41960, #20290, #45724, .T. ) ;
#5495=VERTEX_POINT ( 'NONE', #18243 ) ;
#5501=CARTESIAN_POINT ( 'NONE',  ( 998.9999999999992042, 74.99999999999984368, -359.0000000000000000 ) ) ;
#5513=EDGE_LOOP ( 'NONE', ( #20969, #15897, #8765, #32507 ) ) ;
#5567=ORIENTED_EDGE ( 'NONE', *, *, #13708, .F. ) ;
#5610=DIRECTION ( 'NONE',  ( 0.000000000000000000, 0.000000000000000000, 1.000000000000000000 ) ) ;
#5681=ORIENTED_EDGE ( 'NONE', *, *, #42431, .F. ) ;
#5755=AXIS2_PLACEMENT_3D ( 'NONE', #9642, #28101, #38286 ) ;
#5815=ORIENTED_EDGE ( 'NONE', *, *, #36821, .F. ) ;
#5823=VERTEX_POINT ( 'NONE', #22345 ) ;
#5853=CARTESIAN_POINT ( 'NONE',  ( 998.9999999999992042, -599.0000000000001137, -360.0000000000000000 ) ) ;
#5854=VERTEX_POINT ( 'NONE', #26662 ) ;
#5933=ORIENTED_EDGE ( 'NONE', *, *, #35629, .F. ) ;
#5961=VERTEX_POINT ( 'NONE', #40759 ) ;
#5973=FACE_OUTER_BOUND ( 'NONE', #17101, .T. ) ;
#6037=EDGE_CURVE ( 'NONE', #42633, #5448, #25612, .T. ) ;
#6074=VERTEX_POINT ( 'NONE', #6106 ) ;
#6075=DIRECTION ( 'NONE',  ( 1.000000000000000000, 0.000000000000000000, 0.000000000000000000 ) ) ;
#6079=ORIENTED_EDGE ( 'NONE', *, *, #38013, .T. ) ;
#6106=CARTESIAN_POINT ( 'NONE',  ( 939.9999999999992042, 56.60618624968560653, -350.0000000000000000 ) ) ;
#6199=ORIENTED_EDGE ( 'NONE', *, *, #11210, .F. ) ;
#6213=VECTOR ( 'NONE', #15908, 1000.000000000000114 ) ;
#6270=VECTOR ( 'NONE', #10375, 1000.000000000000000 ) ;
#6326=PRODUCT ( 'MirrorHeavy Cast Iron Table Bed Base', 'MirrorHeavy Cast Iron Table Bed Base', '', ( #21430 ) ) ;
#6355=EDGE_CURVE ( 'NONE', #15790, #30506, #3097, .T. ) ;
#6363=DIRECTION ( 'NONE',  ( 0.000000000000000000, -0.7651688349527138167, -0.6438296778008192334 ) ) ;
#6366=ORIENTED_EDGE ( 'NONE', *, *, #8029, .T. ) ;
#6377=EDGE_CURVE ( 'NONE', #5448, #8915, #17188, .T. ) ;
#6389=VECTOR ( 'NONE', #40428, 1000.000000000000114 ) ;
#6395=AXIS2_PLACEMENT_3D ( 'NONE', #25603, #43592, #39238 ) ;
#6400=EDGE_CURVE ( 'NONE', #3030, #22719, #35200, .T. ) ;
#6403=CARTESIAN_POINT ( 'NONE',  ( 879.9999999999992042, 99.99999999999984368, -360.0000000000000000 ) ) ;
#6406=ADVANCED_FACE ( 'NONE', ( #24335 ), #45145, .T. ) ;
#6424=ORIENTED_EDGE ( 'NONE', *, *, #29246, .T. ) ;
#6428=CARTESIAN_POINT ( 'NONE',  ( 919.9999999999993179, 154.9999999999998863, -360.0000000000000000 ) ) ;
#6450=LINE ( 'NONE', #17537, #34376 ) ;
#6460=CONICAL_SURFACE ( 'NONE', #24882, 8.024999999999948841, 0.7853981633963380560 ) ;
#6515=AXIS2_PLACEMENT_3D ( 'NONE', #6852, #20257, #41983 ) ;
#6529=EDGE_LOOP ( 'NONE', ( #14692, #21309 ) ) ;
#6560=CARTESIAN_POINT ( 'NONE',  ( 914.9999999999992042, 99.99999999999984368, -350.0000000000000000 ) ) ;
#6577=EDGE_CURVE ( 'NONE', #20722, #29177, #35600, .T. ) ;
#6581=VECTOR ( 'NONE', #18741, 1000.000000000000000 ) ;
#6723=ORIENTED_EDGE ( 'NONE', *, *, #39390, .T. ) ;
#6736=DIRECTION ( 'NONE',  ( 1.000000000000000000, 0.000000000000000000, 0.000000000000000000 ) ) ;
#6765=ORIENTED_EDGE ( 'NONE', *, *, #41342, .T. ) ;
#6815=ORIENTED_EDGE ( 'NONE', *, *, #2421, .T. ) ;
#6831=ORIENTED_EDGE ( 'NONE', *, *, #13708, .T. ) ;
#6852=CARTESIAN_POINT ( 'NONE',  ( 919.9999999999993179, 219.9999999999998863, -360.0000000000000000 ) ) ;
#6854=VERTEX_POINT ( 'NONE', #11179 ) ;
#6879=ADVANCED_FACE ( 'NONE', ( #36114 ), #42817, .F. ) ;
#6890=VERTEX_POINT ( 'NONE', #14422 ) ;
#6895=CARTESIAN_POINT ( 'NONE',  ( 927.9999999999992042, 219.9999999999998863, -360.0000000000000000 ) ) ;
#6936=ORIENTED_EDGE ( 'NONE', *, *, #15003, .T. ) ;
#6962=CARTESIAN_POINT ( 'NONE',  ( 939.9999999999993179, -590.0000000000001137, 201.9999999999998579 ) ) ;
#7015=DIRECTION ( 'NONE',  ( 0.000000000000000000, -0.6594541114781790059, -0.7517448203044204691 ) ) ;
#7021=FACE_BOUND ( 'NONE', #21478, .T. ) ;
#7030=CARTESIAN_POINT ( 'NONE',  ( 879.9999999999990905, 479.9999999999998863, 210.0000000000000000 ) ) ;
#7047=CARTESIAN_POINT ( 'NONE',  ( 939.9999999999992042, 62.85347435602262323, -357.4246812887967621 ) ) ;
#7051=ORIENTED_EDGE ( 'NONE', *, *, #39058, .F. ) ;
#7084=DIRECTION ( 'NONE',  ( 1.000000000000000000, 0.000000000000000000, 0.000000000000000000 ) ) ;
#7117=ORIENTED_EDGE ( 'NONE', *, *, #32297, .F. ) ;
#7124=ORIENTED_EDGE ( 'NONE', *, *, #43627, .T. ) ;
#7139=LINE ( 'NONE', #19905, #34404 ) ;
#7191=AXIS2_PLACEMENT_3D ( 'NONE', #40056, #22718, #36812 ) ;
#7195=EDGE_CURVE ( 'NONE', #15686, #1155, #33545, .T. ) ;
#7213=CARTESIAN_POINT ( 'NONE',  ( 187.1337867209877857, -179.7356316342496143, -69.11609595480014434 ) ) ;
#7216=EDGE_CURVE ( 'NONE', #3415, #14853, #16002, .T. ) ;
#7241=ORIENTED_EDGE ( 'NONE', *, *, #29695, .F. ) ;
#7256=CARTESIAN_POINT ( 'NONE',  ( 879.9999999999992042, 479.9999999999998863, 210.0000000000000000 ) ) ;
#7260=DIRECTION ( 'NONE',  ( 0.000000000000000000, 0.000000000000000000, -1.000000000000000000 ) ) ;
#7281=DIRECTION ( 'NONE',  ( 0.000000000000000000, 0.000000000000000000, -1.000000000000000000 ) ) ;
#7317=CARTESIAN_POINT ( 'NONE',  ( 989.9999999999992042, -590.0000000000001137, -360.0000000000000000 ) ) ;
#7323=DIRECTION ( 'NONE',  ( -0.000000000000000000, -0.000000000000000000, 1.000000000000000000 ) ) ;
#7370=FACE_OUTER_BOUND ( 'NONE', #43640, .T. ) ;
#7386=DIRECTION ( 'NONE',  ( -1.000000000000000000, 0.000000000000000000, 0.000000000000000000 ) ) ;
#7402=DIRECTION ( 'NONE',  ( -0.000000000000000000, -0.000000000000000000, 1.000000000000000000 ) ) ;
#7450=EDGE_LOOP ( 'NONE', ( #23019, #42379, #13587, #39320 ) ) ;
#7461=EDGE_LOOP ( 'NONE', ( #36375, #36614, #41484, #42094 ) ) ;
#7541=CARTESIAN_POINT ( 'NONE',  ( 187.1337867209877857, -422.8782571739196783, 207.4246812887968190 ) ) ;
#7555=PLANE ( 'NONE',  #29280 ) ;
#7558=VECTOR ( 'NONE', #34734, 1000.000000000000000 ) ;
#7597=ORIENTED_EDGE ( 'NONE', *, *, #29470, .F. ) ;
#7606=VECTOR ( 'NONE', #37984, 1000.000000000000000 ) ;
#7626=CARTESIAN_POINT ( 'NONE',  ( 998.9999999999992042, 479.9999999999998863, 199.9999999999999716 ) ) ;
#7652=FACE_OUTER_BOUND ( 'NONE', #4893, .T. ) ;
#7697=CARTESIAN_POINT ( 'NONE',  ( 999.9999999999992042, -599.5857864376268935, 359.5857864376268935 ) ) ;
#7722=CARTESIAN_POINT ( 'NONE',  ( 939.9999999999993179, -600.0000000000001137, 360.0000000000000000 ) ) ;
#7729=CARTESIAN_POINT ( 'NONE',  ( 939.9999999999993179, 56.78581973499407809, 212.6378164459127618 ) ) ;
#7730=ADVANCED_FACE ( 'NONE', ( #11120 ), #43215, .F. ) ;
#7755=CARTESIAN_POINT ( 'NONE',  ( 989.9999999999992042, 46.15097736693707020, -350.0000000000000000 ) ) ;
#7765=LINE ( 'NONE', #7317, #20438 ) ;
#7773=ADVANCED_FACE ( 'NONE', ( #11349 ), #25427, .F. ) ;
#7787=CARTESIAN_POINT ( 'NONE',  ( 879.9999999999992042, 249.9999999999998295, -360.0000000000000000 ) ) ;
#7816=EDGE_CURVE ( 'NONE', #19677, #28770, #22488, .T. ) ;
#7865=ORIENTED_EDGE ( 'NONE', *, *, #26116, .F. ) ;
#7872=LINE ( 'NONE', #35333, #40454 ) ;
#7886=CARTESIAN_POINT ( 'NONE',  ( 939.9999999999993179, -600.0000000000001137, -350.0000000000000000 ) ) ;
#7900=CARTESIAN_POINT ( 'NONE',  ( 914.9999999999992042, 74.99999999999984368, -350.0000000000000000 ) ) ;
#7929=ORIENTED_EDGE ( 'NONE', *, *, #28639, .T. ) ;
#7976=ORIENTED_EDGE ( 'NONE', *, *, #31749, .T. ) ;
#8005=CARTESIAN_POINT ( 'NONE',  ( 914.9999999999992042, 74.99999999999984368, -350.0000000000000000 ) ) ;
#8026=DIRECTION ( 'NONE',  ( 1.000000000000000000, 0.000000000000000000, 0.000000000000000000 ) ) ;
#8029=EDGE_CURVE ( 'NONE', #28334, #23746, #19187, .T. ) ;
#8056=EDGE_CURVE ( 'NONE', #15471, #14977, #5310, .T. ) ;
#8154=VERTEX_POINT ( 'NONE', #9919 ) ;
#8213=LINE ( 'NONE', #11004, #31434 ) ;
#8317=VERTEX_POINT ( 'NONE', #23759 ) ;
#8361=ORIENTED_EDGE ( 'NONE', *, *, #11177, .F. ) ;
#8372=ORIENTED_EDGE ( 'NONE', *, *, #15989, .F. ) ;
#8375=AXIS2_PLACEMENT_3D ( 'NONE', #18878, #40110, #8473 ) ;
#8382=DIRECTION ( 'NONE',  ( 1.000000000000000000, 0.000000000000000000, 0.000000000000000000 ) ) ;
#8464=VECTOR ( 'NONE', #10258, 1000.000000000000000 ) ;
#8473=DIRECTION ( 'NONE',  ( 1.000000000000000000, 0.000000000000000000, 0.000000000000000000 ) ) ;
#8517=PLANE ( 'NONE',  #21757 ) ;
#8558=CARTESIAN_POINT ( 'NONE',  ( 914.9999999999992042, 74.99999999999984368, 350.0000000000000000 ) ) ;
#8562=EDGE_LOOP ( 'NONE', ( #27846, #24077, #27537, #18545 ) ) ;
#8583=AXIS2_PLACEMENT_3D ( 'NONE', #44558, #33473, #26541 ) ;
#8608=VERTEX_POINT ( 'NONE', #44736 ) ;
#8645=DIRECTION ( 'NONE',  ( 1.000000000000000000, 0.000000000000000000, 0.000000000000000000 ) ) ;
#8646=EDGE_CURVE ( 'NONE', #16202, #3030, #26934, .T. ) ;
#8663=EDGE_LOOP ( 'NONE', ( #22933, #43468, #1007, #24998 ) ) ;
#8666=VECTOR ( 'NONE', #20195, 1000.000000000000000 ) ;
#8673=ORIENTED_EDGE ( 'NONE', *, *, #42479, .F. ) ;
#8675=CYLINDRICAL_SURFACE ( 'NONE', #29984, 7.999999999999896083 ) ;
#8679=LINE ( 'NONE', #22743, #12814 ) ;
#8701=CARTESIAN_POINT ( 'NONE',  ( 939.9999999999992042, 240.0000000000000568, 201.9999999999999716 ) ) ;
#8765=ORIENTED_EDGE ( 'NONE', *, *, #20717, .F. ) ;
#8767=VECTOR ( 'NONE', #11813, 1000.000000000000000 ) ;
#8797=( NAMED_UNIT ( * ) SI_UNIT ( $, .STERADIAN. ) SOLID_ANGLE_UNIT ( ) );
#8838=CARTESIAN_POINT ( 'NONE',  ( 998.9999999999992042, -600.0000000000001137, -360.0000000000000000 ) ) ;
#8842=EDGE_CURVE ( 'NONE', #8317, #16303, #16093, .T. ) ;
#8876=ORIENTED_EDGE ( 'NONE', *, *, #34864, .T. ) ;
#8884=CARTESIAN_POINT ( 'NONE',  ( 1820.038553321469863, -589.9999999999998863, 201.9999999999998579 ) ) ;
#8889=EDGE_CURVE ( 'NONE', #38409, #20274, #36550, .T. ) ;
#8893=DIRECTION ( 'NONE',  ( 0.000000000000000000, 0.000000000000000000, -1.000000000000000000 ) ) ;
#8915=VERTEX_POINT ( 'NONE', #23913 ) ;
#8947=CARTESIAN_POINT ( 'NONE',  ( 879.9999999999992042, 469.9999999999998863, 210.0000000000000000 ) ) ;
#9036=ORIENTED_EDGE ( 'NONE', *, *, #16099, .F. ) ;
#9096=FACE_OUTER_BOUND ( 'NONE', #30862, .T. ) ;
#9101=CARTESIAN_POINT ( 'NONE',  ( 989.9999999999992042, -590.0000000000001137, 201.9999999999998579 ) ) ;
#9113=CARTESIAN_POINT ( 'NONE',  ( 999.9999999999992042, 248.9999999999998863, 200.9999999999999432 ) ) ;
#9144=ORIENTED_EDGE ( 'NONE', *, *, #22713, .T. ) ;
#9152=ORIENTED_EDGE ( 'NONE', *, *, #8029, .F. ) ;
#9175=CIRCLE ( 'NONE', #43112, 7.999999999999785061 ) ;
#9184=CARTESIAN_POINT ( 'NONE',  ( 187.1337867209877857, 56.73212367640085318, -362.5753187112032379 ) ) ;
#9195=VERTEX_POINT ( 'NONE', #7755 ) ;
#9210=EDGE_LOOP ( 'NONE', ( #13305, #2147, #4895, #43480 ) ) ;
#9266=VECTOR ( 'NONE', #1677, 1000.000000000000000 ) ;
#9270=AXIS2_PLACEMENT_3D ( 'NONE', #13806, #45446, #34798 ) ;
#9351=CARTESIAN_POINT ( 'NONE',  ( 939.9999999999992042, -185.0721577059061929, -75.19946970736496894 ) ) ;
#9372=LINE ( 'NONE', #8701, #42396 ) ;
#9396=DIRECTION ( 'NONE',  ( -1.058954862565134068E-16, 0.6438296778008191223, -0.7651688349527137056 ) ) ;
#9407=LINE ( 'NONE', #31329, #11262 ) ;
#9419=EDGE_LOOP ( 'NONE', ( #28813, #24598, #19852, #26539, #36879, #17634 ) ) ;
#9457=PLANE ( 'NONE',  #18937 ) ;
#9480=FACE_OUTER_BOUND ( 'NONE', #7461, .T. ) ;
#9520=AXIS2_PLACEMENT_3D ( 'NONE', #38807, #7386, #38562 ) ;
#9522=EDGE_CURVE ( 'NONE', #6890, #27336, #35928, .T. ) ;
#9552=ORIENTED_EDGE ( 'NONE', *, *, #13110, .F. ) ;
#9556=CARTESIAN_POINT ( 'NONE',  ( 919.9999999999993179, 154.9999999999998863, 360.0000000000000000 ) ) ;
#9573=EDGE_LOOP ( 'NONE', ( #41204, #29943, #39340, #4392 ) ) ;
#9599=LINE ( 'NONE', #7047, #26961 ) ;
#9600=CARTESIAN_POINT ( 'NONE',  ( 187.1337867209877857, 62.85347435602256638, -357.4246812887967053 ) ) ;
#9642=CARTESIAN_POINT ( 'NONE',  ( 989.9999999999992042, 249.9999999999998863, -360.0000000000000000 ) ) ;
#9717=DIRECTION ( 'NONE',  ( 0.000000000000000000, -0.7517448203044211352, 0.6594541114781782287 ) ) ;
#9718=ORIENTED_EDGE ( 'NONE', *, *, #27310, .F. ) ;
#9747=CARTESIAN_POINT ( 'NONE',  ( 989.9999999999992042, 249.9999999999998863, -360.0000000000000000 ) ) ;
#9776=ADVANCED_FACE ( 'NONE', ( #9096 ), #1698, .F. ) ;
#9777=ORIENTED_EDGE ( 'NONE', *, *, #39309, .F. ) ;
#9791=CARTESIAN_POINT ( 'NONE',  ( 939.9999999999992042, 62.85347435602262323, -357.4246812887967621 ) ) ;
#9809=( GEOMETRIC_REPRESENTATION_CONTEXT ( 3 ) GLOBAL_UNCERTAINTY_ASSIGNED_CONTEXT ( ( #19472 ) ) GLOBAL_UNIT_ASSIGNED_CONTEXT ( ( #1202, #4896, #35616 ) ) REPRESENTATION_CONTEXT ( 'NONE', 'WORKASPACE' ) );
#9819=DIRECTION ( 'NONE',  ( -0.000000000000000000, -1.000000000000000000, 0.000000000000000000 ) ) ;
#9857=VERTEX_POINT ( 'NONE', #33586 ) ;
#9878=CARTESIAN_POINT ( 'NONE',  ( 999.9999999999992042, 478.9999999999999432, 200.9999999999999432 ) ) ;
#9908=ORIENTED_EDGE ( 'NONE', *, *, #16809, .F. ) ;
#9919=CARTESIAN_POINT ( 'NONE',  ( 911.9999999999993179, 154.9999999999998863, -350.0000000000000000 ) ) ;
#9928=VECTOR ( 'NONE', #19460, 1000.000000000000000 ) ;
#9941=EDGE_CURVE ( 'NONE', #23746, #577, #43528, .T. ) ;
#9967=PLANE ( 'NONE',  #11450 ) ;
#10001=ORIENTED_EDGE ( 'NONE', *, *, #22731, .F. ) ;
#10008=ORIENTED_EDGE ( 'NONE', *, *, #35689, .F. ) ;
#10009=VECTOR ( 'NONE', #34332, 999.9999999999998863 ) ;
#10027=DIRECTION ( 'NONE',  ( 0.000000000000000000, 0.7517448203044204691, -0.6594541114781790059 ) ) ;
#10032=PLANE ( 'NONE',  #12098 ) ;
#10045=ADVANCED_FACE ( 'NONE', ( #24088 ), #37736, .F. ) ;
#10141=FACE_OUTER_BOUND ( 'NONE', #11002, .T. ) ;
#10258=DIRECTION ( 'NONE',  ( 1.644774851296528363E-16, -1.000000000000000000, 0.000000000000000000 ) ) ;
#10268=FACE_OUTER_BOUND ( 'NONE', #33046, .T. ) ;
#10314=CARTESIAN_POINT ( 'NONE',  ( 989.9999999999992042, -431.4567479753240491, -350.0000000000000000 ) ) ;
#10316=EDGE_CURVE ( 'NONE', #6854, #12114, #27649, .T. ) ;
#10375=DIRECTION ( 'NONE',  ( 0.000000000000000000, 1.000000000000000000, 0.000000000000000000 ) ) ;
#10397=CARTESIAN_POINT ( 'NONE',  ( 1820.038553321469863, -418.3138125091624602, 201.9999999999998863 ) ) ;
#10426=FACE_OUTER_BOUND ( 'NONE', #30621, .T. ) ;
#10432=CARTESIAN_POINT ( 'NONE',  ( 939.9999999999993179, -590.0000000000001137, 350.0000000000000000 ) ) ;
#10457=ORIENTED_EDGE ( 'NONE', *, *, #11411, .T. ) ;
#10460=ORIENTED_EDGE ( 'NONE', *, *, #13110, .T. ) ;
#10465=DIRECTION ( 'NONE',  ( 0.000000000000000000, 0.000000000000000000, -1.000000000000000000 ) ) ;
#10472=VECTOR ( 'NONE', #26657, 1000.000000000000000 ) ;
#10497=DIRECTION ( 'NONE',  ( 0.000000000000000000, 1.000000000000000000, 0.000000000000000000 ) ) ;
#10529=CARTESIAN_POINT ( 'NONE',  ( 919.9999999999993179, 154.9999999999998863, -350.0000000000000000 ) ) ;
#10534=DIRECTION ( 'NONE',  ( -0.000000000000000000, -0.000000000000000000, 1.000000000000000000 ) ) ;
#10555=EDGE_LOOP ( 'NONE', ( #41763, #44941, #21271, #4285 ) ) ;
#10557=VECTOR ( 'NONE', #4078, 1000.000000000000000 ) ;
#10574=VECTOR ( 'NONE', #29706, 1000.000000000000000 ) ;
#10638=ORIENTED_EDGE ( 'NONE', *, *, #3597, .F. ) ;
#10655=CARTESIAN_POINT ( 'NONE',  ( 914.9999999999992042, 99.99999999999984368, -360.0000000000000000 ) ) ;
#10676=DIRECTION ( 'NONE',  ( 0.000000000000000000, -0.6594541114781790059, -0.7517448203044204691 ) ) ;
#10678=ORIENTED_EDGE ( 'NONE', *, *, #41357, .T. ) ;
#10704=ORIENTED_EDGE ( 'NONE', *, *, #21591, .F. ) ;
#10706=PLANE ( 'NONE',  #42521 ) ;
#10720=CARTESIAN_POINT ( 'NONE',  ( 927.9999999999992042, 154.9999999999998863, -360.0000000000000000 ) ) ;
#10766=VERTEX_POINT ( 'NONE', #30286 ) ;
#10772=DIRECTION ( 'NONE',  ( 1.000000000000000000, 0.000000000000000000, 0.000000000000000000 ) ) ;
#10773=DIRECTION ( 'NONE',  ( 0.000000000000000000, 0.000000000000000000, 1.000000000000000000 ) ) ;
#10777=DIRECTION ( 'NONE',  ( -1.084653538143406060E-16, 0.6594541114781790059, 0.7517448203044204691 ) ) ;
#10779=AXIS2_PLACEMENT_3D ( 'NONE', #607, #22072, #14708 ) ;
#10799=LINE ( 'NONE', #32724, #27648 ) ;
#10801=ORIENTED_EDGE ( 'NONE', *, *, #9941, .T. ) ;
#10803=DIRECTION ( 'NONE',  ( 1.000000000000000000, 0.000000000000000000, 0.000000000000000000 ) ) ;
#10807=AXIS2_PLACEMENT_3D ( 'NONE', #22899, #43925, #40480 ) ;
#10819=VECTOR ( 'NONE', #25124, 1000.000000000000000 ) ;
#10833=DIRECTION ( 'NONE',  ( 0.000000000000000000, 0.000000000000000000, -1.000000000000000000 ) ) ;
#10851=VECTOR ( 'NONE', #14648, 1000.000000000000000 ) ;
#10858=AXIS2_PLACEMENT_3D ( 'NONE', #10529, #24605, #7084 ) ;
#10862=EDGE_CURVE ( 'NONE', #2789, #8317, #11844, .T. ) ;
#10865=EDGE_CURVE ( 'NONE', #41883, #30506, #11566, .T. ) ;
#10872=CARTESIAN_POINT ( 'NONE',  ( 939.9999999999993179, -422.8782571739196214, 207.4246812887968758 ) ) ;
#10900=EDGE_CURVE ( 'NONE', #14035, #14853, #18778, .T. ) ;
#10927=EDGE_LOOP ( 'NONE', ( #1803, #1367, #20978, #45120 ) ) ;
#10930=VERTEX_POINT ( 'NONE', #12303 ) ;
#10946=EDGE_LOOP ( 'NONE', ( #9036, #43240, #28492, #23204 ) ) ;
#10950=ORIENTED_EDGE ( 'NONE', *, *, #34864, .F. ) ;
#10963=DIRECTION ( 'NONE',  ( 0.000000000000000000, 0.000000000000000000, -1.000000000000000000 ) ) ;
#11002=EDGE_LOOP ( 'NONE', ( #22131, #4292, #35284, #29846 ) ) ;
#11004=CARTESIAN_POINT ( 'NONE',  ( 999.9999999999992042, 239.9999999999998863, 209.9999999999999716 ) ) ;
#11024=DIRECTION ( 'NONE',  ( 0.000000000000000000, 1.000000000000000000, 0.000000000000000000 ) ) ;
#11046=SHAPE_DEFINITION_REPRESENTATION ( #20332, #27662 ) ;
#11120=FACE_OUTER_BOUND ( 'NONE', #25006, .T. ) ;
#11135=ADVANCED_FACE ( 'NONE', ( #20123 ), #24902, .T. ) ;
#11145=DIRECTION ( 'NONE',  ( 1.000000000000000000, 0.000000000000000000, 0.000000000000000000 ) ) ;
#11174=EDGE_CURVE ( 'NONE', #16202, #22885, #23798, .T. ) ;
#11177=EDGE_CURVE ( 'NONE', #1691, #38523, #23356, .T. ) ;
#11179=CARTESIAN_POINT ( 'NONE',  ( 998.9999999999992042, -600.0000000000001137, 360.0000000000000000 ) ) ;
#11210=EDGE_CURVE ( 'NONE', #30506, #19677, #7139, .T. ) ;
#11234=LINE ( 'NONE', #42185, #10557 ) ;
#11238=FACE_OUTER_BOUND ( 'NONE', #27164, .T. ) ;
#11262=VECTOR ( 'NONE', #7323, 1000.000000000000000 ) ;
#11326=AXIS2_PLACEMENT_3D ( 'NONE', #2713, #13803, #20491 ) ;
#11333=DIRECTION ( 'NONE',  ( 0.000000000000000000, 0.000000000000000000, 1.000000000000000000 ) ) ;
#11349=FACE_OUTER_BOUND ( 'NONE', #36146, .T. ) ;
#11411=EDGE_CURVE ( 'NONE', #36456, #8317, #43153, .T. ) ;
#11422=VERTEX_POINT ( 'NONE', #28835 ) ;
#11425=STYLED_ITEM('',(#45744),#2862);
#11450=AXIS2_PLACEMENT_3D ( 'NONE', #23179, #24036, #13897 ) ;
#11465=EDGE_CURVE ( 'NONE', #5169, #15565, #22629, .T. ) ;
#11542=VERTEX_POINT ( 'NONE', #11959 ) ;
#11566=CIRCLE ( 'NONE', #10807, 8.000000000000007105 ) ;
#11576=VECTOR ( 'NONE', #17763, 1000.000000000000000 ) ;
#11615=CIRCLE ( 'NONE', #41844, 7.999999999999896083 ) ;
#11640=CARTESIAN_POINT ( 'NONE',  ( 919.9999999999993179, 154.9999999999998863, -360.0000000000000000 ) ) ;
#11745=VECTOR ( 'NONE', #33495, 1000.000000000000000 ) ;
#11751=CARTESIAN_POINT ( 'NONE',  ( 911.9999999999992042, 154.9999999999998863, -359.9749999999999659 ) ) ;
#11813=DIRECTION ( 'NONE',  ( -1.000000000000000000, -4.625929269271485914E-16, 0.000000000000000000 ) ) ;
#11844=LINE ( 'NONE', #26145, #28506 ) ;
#11869=DIRECTION ( 'NONE',  ( 1.000000000000000000, 0.000000000000000000, 0.000000000000000000 ) ) ;
#11870=LINE ( 'NONE', #16235, #30658 ) ;
#11873=ORIENTED_EDGE ( 'NONE', *, *, #43315, .T. ) ;
#11917=CARTESIAN_POINT ( 'NONE',  ( 911.9999999999994316, 219.9999999999998863, 360.0000000000000000 ) ) ;
#11941=ORIENTED_EDGE ( 'NONE', *, *, #15989, .T. ) ;
#11959=CARTESIAN_POINT ( 'NONE',  ( 989.9999999999992042, -590.0000000000001137, -350.0000000000000000 ) ) ;
#11997=CYLINDRICAL_SURFACE ( 'NONE', #27615, 1.000000000000000888 ) ;
#12009=ORIENTED_EDGE ( 'NONE', *, *, #78, .T. ) ;
#12054=VERTEX_POINT ( 'NONE', #30875 ) ;
#12057=EDGE_LOOP ( 'NONE', ( #43732, #14806, #1924, #36036 ) ) ;
#12084=CARTESIAN_POINT ( 'NONE',  ( 879.9999999999990905, -414.5899773927342835, 210.0000000000000000 ) ) ;
#12097=DIRECTION ( 'NONE',  ( 0.000000000000000000, 0.000000000000000000, -1.000000000000000000 ) ) ;
#12098=AXIS2_PLACEMENT_3D ( 'NONE', #2639, #28029, #42123 ) ;
#12102=ORIENTED_EDGE ( 'NONE', *, *, #39058, .T. ) ;
#12105=UNCERTAINTY_MEASURE_WITH_UNIT (LENGTH_MEASURE( 1.000000000000000082E-05 ), #12261, 'distance_accuracy_value', 'NONE');
#12107=LINE ( 'NONE', #26186, #20466 ) ;
#12114=VERTEX_POINT ( 'NONE', #27871 ) ;
#12150=VECTOR ( 'NONE', #17827, 1000.000000000000000 ) ;
#12189=DIRECTION ( 'NONE',  ( 1.337618101958019798E-16, -1.000000000000000000, 0.000000000000000000 ) ) ;
#12194=ADVANCED_FACE ( 'NONE', ( #13794 ), #31093, .F. ) ;
#12197=VERTEX_POINT ( 'NONE', #17485 ) ;
#12200=AXIS2_PLACEMENT_3D ( 'NONE', #27371, #10497, #38236 ) ;
#12220=VECTOR ( 'NONE', #15862, 1000.000000000000000 ) ;
#12226=ORIENTED_EDGE ( 'NONE', *, *, #37930, .T. ) ;
#12232=ADVANCED_FACE ( 'NONE', ( #17238 ), #3625, .T. ) ;
#12243=FACE_OUTER_BOUND ( 'NONE', #23839, .T. ) ;
#12261=( LENGTH_UNIT ( ) NAMED_UNIT ( * ) SI_UNIT ( .MILLI., .METRE. ) );
#12270=EDGE_CURVE ( 'NONE', #41883, #28770, #31324, .T. ) ;
#12303=CARTESIAN_POINT ( 'NONE',  ( 998.9999999999992042, 479.9999999999999432, 199.9999999999999716 ) ) ;
#12305=VECTOR ( 'NONE', #12189, 1000.000000000000000 ) ;
#12314=DIRECTION ( 'NONE',  ( 1.000000000000000000, 0.000000000000000000, 0.000000000000000000 ) ) ;
#12320=VECTOR ( 'NONE', #3686, 1000.000000000000000 ) ;
#12325=VECTOR ( 'NONE', #22573, 1000.000000000000000 ) ;
#12355=DIRECTION ( 'NONE',  ( -1.000000000000000000, 0.000000000000000000, 0.000000000000000000 ) ) ;
#12369=DIRECTION ( 'NONE',  ( -0.000000000000000000, -0.000000000000000000, 1.000000000000000000 ) ) ;
#12416=DIRECTION ( 'NONE',  ( -0.000000000000000000, -0.000000000000000000, 1.000000000000000000 ) ) ;
#12546=ORIENTED_EDGE ( 'NONE', *, *, #36083, .F. ) ;
#12551=PRODUCT_DEFINITION_CONTEXT ( 'detailed design', #36407, 'design' ) ;
#12560=VERTEX_POINT ( 'NONE', #18172 ) ;
#12563=EDGE_CURVE ( 'NONE', #27073, #45131, #36588, .T. ) ;
#12578=CARTESIAN_POINT ( 'NONE',  ( 939.9999999999993179, -416.7569064942979935, 212.5753187112032947 ) ) ;
#12710=CARTESIAN_POINT ( 'NONE',  ( 911.9999999999993179, 219.9999999999998863, 350.0000000000000000 ) ) ;
#12726=VERTEX_POINT ( 'NONE', #1044 ) ;
#12754=DIRECTION ( 'NONE',  ( 1.000000000000000000, 0.000000000000000000, 0.000000000000000000 ) ) ;
#12769=CYLINDRICAL_SURFACE ( 'NONE', #41113, 1.000000000000000888 ) ;
#12774=ORIENTED_EDGE ( 'NONE', *, *, #43315, .F. ) ;
#12790=CARTESIAN_POINT ( 'NONE',  ( 939.9999999999993179, -407.8586036264139807, 201.9999999999998863 ) ) ;
#12791=LINE ( 'NONE', #26647, #18893 ) ;
#12805=ADVANCED_FACE ( 'NONE', ( #29458 ), #44701, .F. ) ;
#12814=VECTOR ( 'NONE', #22953, 1000.000000000000000 ) ;
#12819=CARTESIAN_POINT ( 'NONE',  ( 919.9999999999993179, 154.9999999999998863, -359.9749999999999659 ) ) ;
#12865=CARTESIAN_POINT ( 'NONE',  ( 879.9999999999992042, 99.99999999999984368, -360.0000000000000000 ) ) ;
#12888=EDGE_LOOP ( 'NONE', ( #45405, #20278, #11873, #32537 ) ) ;
#13032=ORIENTED_EDGE ( 'NONE', *, *, #14519, .T. ) ;
#13049=EDGE_CURVE ( 'NONE', #19541, #12560, #8213, .T. ) ;
#13063=DIRECTION ( 'NONE',  ( 0.000000000000000000, 0.000000000000000000, 1.000000000000000000 ) ) ;
#13110=EDGE_CURVE ( 'NONE', #11422, #21201, #12791, .T. ) ;
#13117=CARTESIAN_POINT ( 'NONE',  ( 879.9999999999992042, 239.9999999999998295, 210.0000000000000000 ) ) ;
#13179=DIRECTION ( 'NONE',  ( 0.000000000000000000, -1.000000000000000000, 0.000000000000000000 ) ) ;
#13265=VERTEX_POINT ( 'NONE', #9101 ) ;
#13271=LINE ( 'NONE', #3091, #40843 ) ;
#13276=CARTESIAN_POINT ( 'NONE',  ( 939.9999999999992042, 50.81038600091411439, 217.3872392842761769 ) ) ;
#13289=CARTESIAN_POINT ( 'NONE',  ( 998.9999999999992042, 248.9999999999998863, -360.0000000000000000 ) ) ;
#13298=VERTEX_POINT ( 'NONE', #15807 ) ;
#13305=ORIENTED_EDGE ( 'NONE', *, *, #711, .T. ) ;
#13319=LINE ( 'NONE', #41266, #21102 ) ;
#13327=DIRECTION ( 'NONE',  ( -1.000000000000000000, 0.000000000000000000, 0.000000000000000000 ) ) ;
#13381=ADVANCED_FACE ( 'NONE', ( #26435 ), #8675, .F. ) ;
#13394=EDGE_CURVE ( 'NONE', #13265, #17501, #23412, .T. ) ;
#13402=PLANE ( 'NONE',  #9520 ) ;
#13453=CARTESIAN_POINT ( 'NONE',  ( 999.5857864376259840, -600.0000000000001137, -360.0000000000000000 ) ) ;
#13472=VECTOR ( 'NONE', #31097, 999.9999999999998863 ) ;
#13517=DIRECTION ( 'NONE',  ( 1.000000000000000000, 0.000000000000000000, 0.000000000000000000 ) ) ;
#13522=DIRECTION ( 'NONE',  ( -1.000000000000000000, 0.000000000000000000, 0.000000000000000000 ) ) ;
#13525=ORIENTED_EDGE ( 'NONE', *, *, #31676, .T. ) ;
#13529=FACE_OUTER_BOUND ( 'NONE', #18581, .T. ) ;
#13557=CARTESIAN_POINT ( 'NONE',  ( 927.9999999999992042, 154.9999999999998863, 350.0000000000000000 ) ) ;
#13577=ORIENTED_EDGE ( 'NONE', *, *, #10862, .T. ) ;
#13583=AXIS2_PLACEMENT_3D ( 'NONE', #25244, #31718, #17875 ) ;
#13587=ORIENTED_EDGE ( 'NONE', *, *, #20102, .F. ) ;
#13588=ORIENTED_EDGE ( 'NONE', *, *, #21860, .T. ) ;
#13648=EDGE_CURVE ( 'NONE', #4330, #43869, #42119, .T. ) ;
#13666=ADVANCED_FACE ( 'NONE', ( #23857 ), #37973, .F. ) ;
#13677=LINE ( 'NONE', #3739, #12150 ) ;
#13684=CIRCLE ( 'NONE', #43902, 7.999999999999896083 ) ;
#13705=EDGE_LOOP ( 'NONE', ( #5815, #22452, #37020, #17621 ) ) ;
#13708=EDGE_CURVE ( 'NONE', #20290, #1691, #17421, .T. ) ;
#13782=CIRCLE ( 'NONE', #39610, 24.99999999999991118 ) ;
#13794=FACE_OUTER_BOUND ( 'NONE', #16209, .T. ) ;
#13803=DIRECTION ( 'NONE',  ( 0.000000000000000000, 0.000000000000000000, -1.000000000000000000 ) ) ;
#13806=CARTESIAN_POINT ( 'NONE',  ( 919.9999999999993179, 154.9999999999998863, -360.0000000000000000 ) ) ;
#13844=DIRECTION ( 'NONE',  ( -0.000000000000000000, -0.7517448203044211352, 0.6594541114781783397 ) ) ;
#13881=VECTOR ( 'NONE', #24179, 1000.000000000000000 ) ;
#13897=DIRECTION ( 'NONE',  ( 0.000000000000000000, -0.6438296778008192334, 0.7651688349527138167 ) ) ;
#13954=FACE_BOUND ( 'NONE', #14575, .T. ) ;
#13956=ADVANCED_FACE ( 'NONE', ( #12243, #22848, #25239 ), #39349, .T. ) ;
#13961=ADVANCED_FACE ( 'NONE', ( #28243, #42589, #32187 ), #10706, .F. ) ;
#13974=EDGE_CURVE ( 'NONE', #5961, #43956, #35878, .T. ) ;
#13981=LINE ( 'NONE', #34979, #14415 ) ;
#14018=FACE_OUTER_BOUND ( 'NONE', #40567, .T. ) ;
#14035=VERTEX_POINT ( 'NONE', #18343 ) ;
#14042=ORIENTED_EDGE ( 'NONE', *, *, #6577, .F. ) ;
#14132=CARTESIAN_POINT ( 'NONE',  ( 879.9999999999990905, 50.81038600091414281, 210.0000000000000000 ) ) ;
#14157=ORIENTED_EDGE ( 'NONE', *, *, #27840, .T. ) ;
#14169=EDGE_CURVE ( 'NONE', #13298, #33885, #13782, .T. ) ;
#14174=DIRECTION ( 'NONE',  ( 0.000000000000000000, 0.000000000000000000, 1.000000000000000000 ) ) ;
#14184=DIRECTION ( 'NONE',  ( 0.000000000000000000, 0.000000000000000000, -1.000000000000000000 ) ) ;
#14208=DIRECTION ( 'NONE',  ( 1.000000000000000000, 0.000000000000000000, 0.000000000000000000 ) ) ;
#14210=VERTEX_POINT ( 'NONE', #23061 ) ;
#14219=ORIENTED_EDGE ( 'NONE', *, *, #6037, .F. ) ;
#14287=FACE_OUTER_BOUND ( 'NONE', #29742, .T. ) ;
#14308=CARTESIAN_POINT ( 'NONE',  ( 989.9999999999992042, 56.60618624968560653, -350.0000000000000000 ) ) ;
#14321=ADVANCED_FACE ( 'NONE', ( #10141 ), #39019, .T. ) ;
#14346=VECTOR ( 'NONE', #13063, 1000.000000000000000 ) ;
#14370=LINE ( 'NONE', #28451, #4080 ) ;
#14411=ORIENTED_EDGE ( 'NONE', *, *, #39421, .F. ) ;
#14415=VECTOR ( 'NONE', #9819, 1000.000000000000000 ) ;
#14422=CARTESIAN_POINT ( 'NONE',  ( 989.9999999999992042, 239.9999999999998863, -350.0000000000000000 ) ) ;
#14439=LINE ( 'NONE', #795, #16618 ) ;
#14519=EDGE_CURVE ( 'NONE', #9857, #31480, #45486, .T. ) ;
#14534=CARTESIAN_POINT ( 'NONE',  ( 879.9999999999992042, 249.9999999999998295, -360.0000000000000000 ) ) ;
#14548=VECTOR ( 'NONE', #12416, 1000.000000000000000 ) ;
#14575=EDGE_LOOP ( 'NONE', ( #12774, #23728, #18552 ) ) ;
#14635=EDGE_LOOP ( 'NONE', ( #25745, #32042, #29120, #37724, #23709, #5933 ) ) ;
#14648=DIRECTION ( 'NONE',  ( 1.000000000000000000, 0.000000000000000000, 0.000000000000000000 ) ) ;
#14692=ORIENTED_EDGE ( 'NONE', *, *, #26628, .T. ) ;
#14708=DIRECTION ( 'NONE',  ( 1.000000000000000000, 0.000000000000000000, 0.000000000000000000 ) ) ;
#14757=EDGE_CURVE ( 'NONE', #43956, #15632, #29067, .T. ) ;
#14796=FACE_OUTER_BOUND ( 'NONE', #9210, .T. ) ;
#14806=ORIENTED_EDGE ( 'NONE', *, *, #37084, .F. ) ;
#14812=DIRECTION ( 'NONE',  ( 0.000000000000000000, 0.000000000000000000, 1.000000000000000000 ) ) ;
#14816=ORIENTED_EDGE ( 'NONE', *, *, #22713, .F. ) ;
#14824=DIRECTION ( 'NONE',  ( 4.625929269271485914E-16, -1.000000000000000000, 0.000000000000000000 ) ) ;
#14853=VERTEX_POINT ( 'NONE', #36439 ) ;
#14859=EDGE_CURVE ( 'NONE', #17002, #12726, #25360, .T. ) ;
#14873=LINE ( 'NONE', #22015, #4223 ) ;
#14879=CARTESIAN_POINT ( 'NONE',  ( 989.9999999999992042, 249.9999999999998863, 209.9999999999999716 ) ) ;
#14913=EDGE_LOOP ( 'NONE', ( #21303, #33985, #19565, #21370, #43910, #5047, #34769, #31307, #23342, #27099, #4103, #5567, #21607 ) ) ;
#14934=CYLINDRICAL_SURFACE ( 'NONE', #22378, 7.999999999999896083 ) ;
#14976=DIRECTION ( 'NONE',  ( 1.000000000000000000, 0.000000000000000000, 0.000000000000000000 ) ) ;
#14977=VERTEX_POINT ( 'NONE', #41279 ) ;
#15003=EDGE_CURVE ( 'NONE', #27925, #40626, #26948, .T. ) ;
#15038=PLANE ( 'NONE',  #17220 ) ;
#15095=CARTESIAN_POINT ( 'NONE',  ( 879.9999999999992042, 99.99999999999984368, 350.0000000000000000 ) ) ;
#15154=CARTESIAN_POINT ( 'NONE',  ( 919.9999999999993179, 154.9999999999998863, 350.0000000000000000 ) ) ;
#15162=AXIS2_PLACEMENT_3D ( 'NONE', #27088, #44400, #12754 ) ;
#15165=FACE_OUTER_BOUND ( 'NONE', #7450, .T. ) ;
#15194=VERTEX_POINT ( 'NONE', #23246 ) ;
#15199=EDGE_LOOP ( 'NONE', ( #1423, #4825, #2515, #37608 ) ) ;
#15218=LINE ( 'NONE', #28610, #10819 ) ;
#15286=DIRECTION ( 'NONE',  ( 1.000000000000000000, 0.000000000000000000, 0.000000000000000000 ) ) ;
#15288=DIRECTION ( 'NONE',  ( 1.000000000000000000, 0.000000000000000000, 0.000000000000000000 ) ) ;
#15290=LINE ( 'NONE', #4434, #8767 ) ;
#15349=PLANE ( 'NONE',  #22504 ) ;
#15392=DIRECTION ( 'NONE',  ( 0.000000000000000000, -1.000000000000000000, -1.672022627447525240E-16 ) ) ;
#15414=DIRECTION ( 'NONE',  ( 0.000000000000000000, 0.000000000000000000, -1.000000000000000000 ) ) ;
#15445=LINE ( 'NONE', #29522, #25980 ) ;
#15471=VERTEX_POINT ( 'NONE', #31568 ) ;
#15477=ORIENTED_EDGE ( 'NONE', *, *, #41497, .T. ) ;
#15557=LINE ( 'NONE', #1670, #35773 ) ;
#15565=VERTEX_POINT ( 'NONE', #13557 ) ;
#15607=CARTESIAN_POINT ( 'NONE',  ( 989.9999999999992042, 469.9999999999999432, 210.0000000000000000 ) ) ;
#15628=EDGE_CURVE ( 'NONE', #5961, #42633, #149, .T. ) ;
#15630=ORIENTED_EDGE ( 'NONE', *, *, #10865, .T. ) ;
#15632=VERTEX_POINT ( 'NONE', #10314 ) ;
#15648=EDGE_CURVE ( 'NONE', #5823, #26364, #24386, .T. ) ;
#15655=ORIENTED_EDGE ( 'NONE', *, *, #37723, .T. ) ;
#15670=ORIENTED_EDGE ( 'NONE', *, *, #22881, .T. ) ;
#15686=VERTEX_POINT ( 'NONE', #1498 ) ;
#15697=ORIENTED_EDGE ( 'NONE', *, *, #30109, .T. ) ;
#15790=VERTEX_POINT ( 'NONE', #32942 ) ;
#15797=AXIS2_PLACEMENT_3D ( 'NONE', #9747, #21286, #24503 ) ;
#15798=ORIENTED_EDGE ( 'NONE', *, *, #24975, .F. ) ;
#15807=CARTESIAN_POINT ( 'NONE',  ( 914.9999999999992042, 99.99999999999984368, 350.0000000000000000 ) ) ;
#15822=CARTESIAN_POINT ( 'NONE',  ( 939.9999999999993179, -414.5899773927343404, 210.0000000000000000 ) ) ;
#15862=DIRECTION ( 'NONE',  ( 1.000000000000000000, 4.625929269271485914E-16, 0.000000000000000000 ) ) ;
#15876=CARTESIAN_POINT ( 'NONE',  ( 928.0249999999991815, 219.9999999999998863, -360.0000000000000000 ) ) ;
#15897=ORIENTED_EDGE ( 'NONE', *, *, #31160, .T. ) ;
#15908=DIRECTION ( 'NONE',  ( -0.000000000000000000, -0.6438296778008192334, 0.7651688349527135946 ) ) ;
#15913=( BOUNDED_CURVE ( )  B_SPLINE_CURVE ( 3, ( #22302, #19922, #13453, #34465 ),
 .UNSPECIFIED., .F., .T. ) 
 B_SPLINE_CURVE_WITH_KNOTS ( ( 4, 4 ),
 ( 4.712388980384689674, 6.283185307179586232 ),
 .UNSPECIFIED. ) 
 CURVE ( )  GEOMETRIC_REPRESENTATION_ITEM ( )  RATIONAL_B_SPLINE_CURVE ( ( 1.000000000000000000, 0.8047378541243649375, 0.8047378541243649375, 1.000000000000000000 ) ) 
 REPRESENTATION_ITEM ( '' )  );
#15942=VECTOR ( 'NONE', #14184, 1000.000000000000000 ) ;
#15970=ORIENTED_EDGE ( 'NONE', *, *, #26611, .F. ) ;
#15981=VECTOR ( 'NONE', #42915, 1000.000000000000000 ) ;
#15989=EDGE_CURVE ( 'NONE', #38523, #41960, #20190, .T. ) ;
#16002=LINE ( 'NONE', #1664, #43957 ) ;
#16016=CARTESIAN_POINT ( 'NONE',  ( 187.1337867209877857, -434.4637272565419153, -347.3621835540870961 ) ) ;
#16043=DIRECTION ( 'NONE',  ( -1.000000000000000000, -1.644774851296528363E-16, -0.000000000000000000 ) ) ;
#16079=ORIENTED_EDGE ( 'NONE', *, *, #32297, .T. ) ;
#16093=LINE ( 'NONE', #2224, #12220 ) ;
#16099=EDGE_CURVE ( 'NONE', #20290, #12560, #40753, .T. ) ;
#16111=VECTOR ( 'NONE', #21253, 1000.000000000000114 ) ;
#16202=VERTEX_POINT ( 'NONE', #9351 ) ;
#16209=EDGE_LOOP ( 'NONE', ( #11941, #23740, #6831, #27059 ) ) ;
#16235=CARTESIAN_POINT ( 'NONE',  ( 989.9999999999992042, 239.9999999999998863, -360.0000000000000000 ) ) ;
#16244=FACE_OUTER_BOUND ( 'NONE', #13705, .T. ) ;
#16261=CARTESIAN_POINT ( 'NONE',  ( 879.9999999999992042, 469.9999999999998863, 350.0000000000000000 ) ) ;
#16301=LINE ( 'NONE', #19995, #23081 ) ;
#16303=VERTEX_POINT ( 'NONE', #2643 ) ;
#16325=LINE ( 'NONE', #28083, #22601 ) ;
#16471=EDGE_CURVE ( 'NONE', #12197, #20750, #35416, .T. ) ;
#16493=DIRECTION ( 'NONE',  ( -0.000000000000000000, -0.000000000000000000, 1.000000000000000000 ) ) ;
#16499=CARTESIAN_POINT ( 'NONE',  ( 999.9999999999992042, 249.9999999999998863, 200.9999999999999432 ) ) ;
#16549=AXIS2_PLACEMENT_3D ( 'NONE', #452, #39733, #39497 ) ;
#16581=CARTESIAN_POINT ( 'NONE',  ( 999.9999999999992042, -590.0000000000001137, 350.0000000000000000 ) ) ;
#16592=ORIENTED_EDGE ( 'NONE', *, *, #24578, .T. ) ;
#16618=VECTOR ( 'NONE', #28751, 1000.000000000000000 ) ;
#16635=CARTESIAN_POINT ( 'NONE',  ( 998.9999999999992042, 249.9999999999998863, -360.0000000000000000 ) ) ;
#16674=DIRECTION ( 'NONE',  ( 0.000000000000000000, -0.6594541114781790059, -0.7517448203044204691 ) ) ;
#16691=LINE ( 'NONE', #41401, #29412 ) ;
#16706=AXIS2_PLACEMENT_3D ( 'NONE', #21550, #7260, #33475 ) ;
#16740=CARTESIAN_POINT ( 'NONE',  ( 911.9999999999993179, 219.9999999999998863, -360.0000000000000000 ) ) ;
#16741=CARTESIAN_POINT ( 'NONE',  ( 939.9999999999992042, 240.0000000000000568, 201.9999999999999716 ) ) ;
#16762=PLANE ( 'NONE',  #12200 ) ;
#16770=CARTESIAN_POINT ( 'NONE',  ( 914.9999999999992042, 99.99999999999984368, -350.0000000000000000 ) ) ;
#16801=CARTESIAN_POINT ( 'NONE',  ( 914.9999999999992042, 99.99999999999984368, 360.0000000000000000 ) ) ;
#16809=EDGE_CURVE ( 'NONE', #1277, #15686, #22458, .T. ) ;
#16867=DIRECTION ( 'NONE',  ( 1.000000000000000000, 0.000000000000000000, 0.000000000000000000 ) ) ;
#16879=CARTESIAN_POINT ( 'NONE',  ( 879.9999999999990905, 479.9999999999998863, 199.9999999999999716 ) ) ;
#16888=DIRECTION ( 'NONE',  ( 1.000000000000000000, 2.313994520913686024E-32, -2.750100768424433609E-32 ) ) ;
#16985=PLANE ( 'NONE',  #30623 ) ;
#16993=CARTESIAN_POINT ( 'NONE',  ( 999.9999999999992042, 248.9999999999998863, -360.0000000000000000 ) ) ;
#17002=VERTEX_POINT ( 'NONE', #43035 ) ;
#17038=CARTESIAN_POINT ( 'NONE',  ( 927.9999999999992042, 154.9999999999998863, -360.0000000000000000 ) ) ;
#17079=EDGE_CURVE ( 'NONE', #15790, #8154, #39213, .T. ) ;
#17086=CARTESIAN_POINT ( 'NONE',  ( 919.9999999999993179, 219.9999999999998863, -359.9749999999999659 ) ) ;
#17095=EDGE_CURVE ( 'NONE', #11542, #15632, #19683, .T. ) ;
#17101=EDGE_LOOP ( 'NONE', ( #22617, #3655, #19664, #13588 ) ) ;
#17137=FACE_OUTER_BOUND ( 'NONE', #22598, .T. ) ;
#17169=ORIENTED_EDGE ( 'NONE', *, *, #34208, .F. ) ;
#17184=DIRECTION ( 'NONE',  ( 1.000000000000000000, 0.000000000000000000, 0.000000000000000000 ) ) ;
#17188=LINE ( 'NONE', #31046, #454 ) ;
#17201=ADVANCED_BREP_SHAPE_REPRESENTATION ( '', ( #2862, #26858 ), #9809 ) ;
#17220=AXIS2_PLACEMENT_3D ( 'NONE', #7900, #34962, #17184 ) ;
#17228=DIRECTION ( 'NONE',  ( -0.000000000000000000, -0.000000000000000000, 1.000000000000000000 ) ) ;
#17238=FACE_OUTER_BOUND ( 'NONE', #10946, .T. ) ;
#17264=FACE_BOUND ( 'NONE', #19260, .T. ) ;
#17323=ORIENTED_EDGE ( 'NONE', *, *, #25106, .F. ) ;
#17395=DIRECTION ( 'NONE',  ( 0.000000000000000000, 0.000000000000000000, 1.000000000000000000 ) ) ;
#17408=ORIENTED_EDGE ( 'NONE', *, *, #13648, .F. ) ;
#17412=( BOUNDED_CURVE ( )  B_SPLINE_CURVE ( 3, ( #9113, #27135, #2404, #37055 ),
 .UNSPECIFIED., .F., .T. ) 
 B_SPLINE_CURVE_WITH_KNOTS ( ( 4, 4 ),
 ( 1.570796326794896558, 3.141592653589793116 ),
 .UNSPECIFIED. ) 
 CURVE ( )  GEOMETRIC_REPRESENTATION_ITEM ( )  RATIONAL_B_SPLINE_CURVE ( ( 1.000000000000000000, 0.8047378541243649375, 0.8047378541243649375, 1.000000000000000000 ) ) 
 REPRESENTATION_ITEM ( '' )  );
#17421=LINE ( 'NONE', #31499, #23344 ) ;
#17456=LINE ( 'NONE', #16770, #31964 ) ;
#17473=VECTOR ( 'NONE', #21107, 1000.000000000000114 ) ;
#17485=CARTESIAN_POINT ( 'NONE',  ( 911.9999999999993179, 219.9999999999998863, -350.0000000000000000 ) ) ;
#17498=CARTESIAN_POINT ( 'NONE',  ( 928.0249999999991815, 154.9999999999998863, -360.0000000000000000 ) ) ;
#17501=VERTEX_POINT ( 'NONE', #6962 ) ;
#17507=LINE ( 'NONE', #17038, #34264 ) ;
#17515=VECTOR ( 'NONE', #41420, 1000.000000000000000 ) ;
#17518=AXIS2_PLACEMENT_3D ( 'NONE', #8005, #39188, #18847 ) ;
#17537=CARTESIAN_POINT ( 'NONE',  ( 1820.038553321469863, -589.9999999999998863, 210.0000000000000000 ) ) ;
#17540=LINE ( 'NONE', #6895, #35649 ) ;
#17572=CARTESIAN_POINT ( 'NONE',  ( 914.9999999999992042, 74.99999999999984368, -350.0000000000000000 ) ) ;
#17576=AXIS2_PLACEMENT_3D ( 'NONE', #17572, #31643, #234 ) ;
#17621=ORIENTED_EDGE ( 'NONE', *, *, #21591, .T. ) ;
#17623=ADVANCED_FACE ( 'NONE', ( #7652 ), #28436, .F. ) ;
#17634=ORIENTED_EDGE ( 'NONE', *, *, #711, .F. ) ;
#17662=DIRECTION ( 'NONE',  ( 0.000000000000000000, 0.000000000000000000, 1.000000000000000000 ) ) ;
#17674=ADVANCED_FACE ( 'NONE', ( #22186 ), #3733, .F. ) ;
#17713=CARTESIAN_POINT ( 'NONE',  ( 879.9999999999990905, 479.9999999999998863, 210.0000000000000000 ) ) ;
#17763=DIRECTION ( 'NONE',  ( 1.000000000000000000, 0.000000000000000000, 0.000000000000000000 ) ) ;
#17827=DIRECTION ( 'NONE',  ( -0.000000000000000000, -0.000000000000000000, 1.000000000000000000 ) ) ;
#17846=ADVANCED_FACE ( 'NONE', ( #39297 ), #32373, .T. ) ;
#17875=DIRECTION ( 'NONE',  ( 0.000000000000000000, 0.000000000000000000, -1.000000000000000000 ) ) ;
#17927=DIRECTION ( 'NONE',  ( 1.000000000000000000, 0.000000000000000000, 0.000000000000000000 ) ) ;
#17960=VECTOR ( 'NONE', #26279, 1000.000000000000000 ) ;
#17989=CARTESIAN_POINT ( 'NONE',  ( 989.9999999999992042, 56.78581973499402835, 212.6378164459127049 ) ) ;
#18050=DIRECTION ( 'NONE',  ( 0.000000000000000000, 1.000000000000000000, 0.000000000000000000 ) ) ;
#18084=ORIENTED_EDGE ( 'NONE', *, *, #31160, .F. ) ;
#18141=CARTESIAN_POINT ( 'NONE',  ( 939.9999999999992042, 74.99999999999984368, 350.0000000000000000 ) ) ;
#18170=VECTOR ( 'NONE', #40072, 1000.000000000000000 ) ;
#18172=CARTESIAN_POINT ( 'NONE',  ( 989.9999999999992042, 240.0000000000000568, 210.0000000000000000 ) ) ;
#18196=DIRECTION ( 'NONE',  ( -0.000000000000000000, -0.000000000000000000, 1.000000000000000000 ) ) ;
#18202=DIRECTION ( 'NONE',  ( 1.000000000000000000, 0.000000000000000000, 0.000000000000000000 ) ) ;
#18212=ORIENTED_EDGE ( 'NONE', *, *, #36226, .T. ) ;
#18243=CARTESIAN_POINT ( 'NONE',  ( 989.9999999999992042, -426.1357934546398383, -350.0000000000000000 ) ) ;
#18273=EDGE_LOOP ( 'NONE', ( #24262, #19964 ) ) ;
#18331=ORIENTED_EDGE ( 'NONE', *, *, #33345, .F. ) ;
#18342=CARTESIAN_POINT ( 'NONE',  ( 999.9999999999992042, -600.0000000000001137, 360.0000000000000000 ) ) ;
#18343=CARTESIAN_POINT ( 'NONE',  ( 989.9999999999992042, 50.81038600091411439, 193.6948738798775764 ) ) ;
#18383=EDGE_LOOP ( 'NONE', ( #24195, #9552, #42841, #10704 ) ) ;
#18391=ORIENTED_EDGE ( 'NONE', *, *, #8646, .F. ) ;
#18470=LINE ( 'NONE', #32549, #20231 ) ;
#18498=EDGE_LOOP ( 'NONE', ( #30572, #22263, #36421, #1164, #8876, #26980, #18331 ) ) ;
#18504=ADVANCED_FACE ( 'NONE', ( #14018 ), #25077, .T. ) ;
#18512=CARTESIAN_POINT ( 'NONE',  ( 989.9999999999992042, 62.79977829742938411, 207.3621835540872951 ) ) ;
#18545=ORIENTED_EDGE ( 'NONE', *, *, #26159, .F. ) ;
#18552=ORIENTED_EDGE ( 'NONE', *, *, #31423, .T. ) ;
#18581=EDGE_LOOP ( 'NONE', ( #21312, #15630, #24308, #29750 ) ) ;
#18600=EDGE_LOOP ( 'NONE', ( #18212, #29989 ) ) ;
#18741=DIRECTION ( 'NONE',  ( 1.000000000000000000, 0.000000000000000000, 0.000000000000000000 ) ) ;
#18778=LINE ( 'NONE', #5133, #4187 ) ;
#18793=DIRECTION ( 'NONE',  ( 1.000000000000000000, 0.000000000000000000, 0.000000000000000000 ) ) ;
#18847=DIRECTION ( 'NONE',  ( 1.000000000000000000, 0.000000000000000000, 0.000000000000000000 ) ) ;
#18878=CARTESIAN_POINT ( 'NONE',  ( 919.9999999999993179, 154.9999999999998863, 360.0000000000000000 ) ) ;
#18888=ORIENTED_EDGE ( 'NONE', *, *, #35964, .F. ) ;
#18893=VECTOR ( 'NONE', #16493, 1000.000000000000000 ) ;
#18937=AXIS2_PLACEMENT_3D ( 'NONE', #44098, #1819, #20063 ) ;
#19018=ADVANCED_FACE ( 'NONE', ( #38157 ), #9967, .F. ) ;
#19035=LINE ( 'NONE', #29869, #35072 ) ;
#19059=CARTESIAN_POINT ( 'NONE',  ( 999.9999999999992042, 248.9999999999998863, -359.0000000000000000 ) ) ;
#19062=ORIENTED_EDGE ( 'NONE', *, *, #9522, .T. ) ;
#19111=ORIENTED_EDGE ( 'NONE', *, *, #21005, .F. ) ;
#19128=CARTESIAN_POINT ( 'NONE',  ( 914.9999999999992042, -431.4567479753239354, -350.0000000000000000 ) ) ;
#19131=ORIENTED_EDGE ( 'NONE', *, *, #3316, .T. ) ;
#19172=DIRECTION ( 'NONE',  ( 0.000000000000000000, 0.000000000000000000, -1.000000000000000000 ) ) ;
#19187=LINE ( 'NONE', #26341, #19557 ) ;
#19229=DIRECTION ( 'NONE',  ( -0.000000000000000000, -0.000000000000000000, 1.000000000000000000 ) ) ;
#19244=CARTESIAN_POINT ( 'NONE',  ( 939.9999999999993179, -426.1357934546398383, -350.0000000000000000 ) ) ;
#19255=VERTEX_POINT ( 'NONE', #12578 ) ;
#19260=EDGE_LOOP ( 'NONE', ( #33404, #25154 ) ) ;
#19273=AXIS2_PLACEMENT_3D ( 'NONE', #40489, #19229, #12314 ) ;
#19347=ADVANCED_FACE ( 'NONE', ( #44289 ), #8517, .T. ) ;
#19351=ORIENTED_EDGE ( 'NONE', *, *, #43879, .F. ) ;
#19370=EDGE_CURVE ( 'NONE', #28770, #19677, #22542, .T. ) ;
#19389=FACE_OUTER_BOUND ( 'NONE', #33303, .T. ) ;
#19408=CARTESIAN_POINT ( 'NONE',  ( 989.9999999999992042, 249.9999999999998863, -350.0000000000000000 ) ) ;
#19460=DIRECTION ( 'NONE',  ( 1.000000000000000000, 2.313994520913686024E-32, -2.750100768424433609E-32 ) ) ;
#19472=UNCERTAINTY_MEASURE_WITH_UNIT (LENGTH_MEASURE( 1.000000000000000082E-05 ), #1202, 'distance_accuracy_value', 'NONE');
#19497=CARTESIAN_POINT ( 'NONE',  ( 911.9749999999993406, 219.9999999999998863, -360.0000000000000000 ) ) ;
#19516=CIRCLE ( 'NONE', #15162, 7.999999999999896083 ) ;
#19521=AXIS2_PLACEMENT_3D ( 'NONE', #11640, #4479, #18793 ) ;
#19541=VERTEX_POINT ( 'NONE', #13117 ) ;
#19557=VECTOR ( 'NONE', #26558, 1000.000000000000000 ) ;
#19563=DIRECTION ( 'NONE',  ( 1.000000000000000000, 0.000000000000000000, 0.000000000000000000 ) ) ;
#19565=ORIENTED_EDGE ( 'NONE', *, *, #7216, .T. ) ;
#19595=DIRECTION ( 'NONE',  ( 0.000000000000000000, 0.000000000000000000, 1.000000000000000000 ) ) ;
#19612=ORIENTED_EDGE ( 'NONE', *, *, #9941, .F. ) ;
#19656=ORIENTED_EDGE ( 'NONE', *, *, #27209, .T. ) ;
#19659=VERTEX_POINT ( 'NONE', #37817 ) ;
#19664=ORIENTED_EDGE ( 'NONE', *, *, #13394, .T. ) ;
#19668=ORIENTED_EDGE ( 'NONE', *, *, #15648, .T. ) ;
#19677=VERTEX_POINT ( 'NONE', #17498 ) ;
#19683=LINE ( 'NONE', #4919, #3054 ) ;
#19709=CIRCLE ( 'NONE', #10858, 7.999999999999896083 ) ;
#19750=FACE_OUTER_BOUND ( 'NONE', #24909, .T. ) ;
#19773=CIRCLE ( 'NONE', #6515, 8.024999999999948841 ) ;
#19798=CARTESIAN_POINT ( 'NONE',  ( 911.9749999999993406, 219.9999999999998863, -360.0000000000000000 ) ) ;
#19818=EDGE_LOOP ( 'NONE', ( #15655, #7929, #20228, #44052 ) ) ;
#19830=EDGE_LOOP ( 'NONE', ( #43125, #36485, #15697, #31500 ) ) ;
#19845=PLANE ( 'NONE',  #8583 ) ;
#19852=ORIENTED_EDGE ( 'NONE', *, *, #35972, .F. ) ;
#19876=ADVANCED_FACE ( 'NONE', ( #28573 ), #7555, .T. ) ;
#19885=APPLICATION_CONTEXT ( 'automotive_design' ) ;
#19892=ORIENTED_EDGE ( 'NONE', *, *, #43308, .T. ) ;
#19905=CARTESIAN_POINT ( 'NONE',  ( 928.0249999999991815, 154.9999999999998863, -360.0000000000000000 ) ) ;
#19922=CARTESIAN_POINT ( 'NONE',  ( 999.9999999999992042, -599.5857864376268935, -359.5857864376268935 ) ) ;
#19964=ORIENTED_EDGE ( 'NONE', *, *, #19370, .T. ) ;
#19967=LINE ( 'NONE', #16499, #33725 ) ;
#19971=FACE_OUTER_BOUND ( 'NONE', #33893, .T. ) ;
#19977=PLANE ( 'NONE',  #25459 ) ;
#19984=DIRECTION ( 'NONE',  ( -0.000000000000000000, -0.000000000000000000, 1.000000000000000000 ) ) ;
#19995=CARTESIAN_POINT ( 'NONE',  ( 998.9999999999992042, 74.99999999999984368, 360.0000000000000000 ) ) ;
#20061=ORIENTED_EDGE ( 'NONE', *, *, #22184, .F. ) ;
#20063=DIRECTION ( 'NONE',  ( 0.000000000000000000, -1.000000000000000000, -1.672022627447525240E-16 ) ) ;
#20102=EDGE_CURVE ( 'NONE', #40626, #42174, #22088, .T. ) ;
#20123=FACE_OUTER_BOUND ( 'NONE', #22169, .T. ) ;
#20190=LINE ( 'NONE', #26444, #24472 ) ;
#20195=DIRECTION ( 'NONE',  ( 1.000000000000000000, 0.000000000000000000, 0.000000000000000000 ) ) ;
#20228=ORIENTED_EDGE ( 'NONE', *, *, #11174, .F. ) ;
#20231=VECTOR ( 'NONE', #35540, 1000.000000000000000 ) ;
#20257=DIRECTION ( 'NONE',  ( -0.000000000000000000, -0.000000000000000000, 1.000000000000000000 ) ) ;
#20274=VERTEX_POINT ( 'NONE', #11917 ) ;
#20278=ORIENTED_EDGE ( 'NONE', *, *, #78, .F. ) ;
#20290=VERTEX_POINT ( 'NONE', #15607 ) ;
#20326=VECTOR ( 'NONE', #36585, 1000.000000000000000 ) ;
#20332=PRODUCT_DEFINITION_SHAPE ( 'NONE', 'NONE',  #3610 ) ;
#20347=EDGE_LOOP ( 'NONE', ( #5341, #19656, #30883, #24082 ) ) ;
#20438=VECTOR ( 'NONE', #29008, 1000.000000000000000 ) ;
#20445=CARTESIAN_POINT ( 'NONE',  ( 879.9999999999990905, 479.9999999999998863, 199.9999999999999716 ) ) ;
#20466=VECTOR ( 'NONE', #4951, 1000.000000000000000 ) ;
#20491=DIRECTION ( 'NONE',  ( 1.000000000000000000, 0.000000000000000000, 0.000000000000000000 ) ) ;
#20535=VERTEX_POINT ( 'NONE', #43767 ) ;
#20593=DIRECTION ( 'NONE',  ( -1.000000000000000000, 0.000000000000000000, 0.000000000000000000 ) ) ;
#20668=DIRECTION ( 'NONE',  ( 0.000000000000000000, 0.000000000000000000, -1.000000000000000000 ) ) ;
#20712=EDGE_CURVE ( 'NONE', #10766, #17501, #44702, .T. ) ;
#20717=EDGE_CURVE ( 'NONE', #30506, #41883, #42363, .T. ) ;
#20722=VERTEX_POINT ( 'NONE', #37536 ) ;
#20750=VERTEX_POINT ( 'NONE', #34060 ) ;
#20836=FACE_OUTER_BOUND ( 'NONE', #39457, .T. ) ;
#20846=ORIENTED_EDGE ( 'NONE', *, *, #10865, .F. ) ;
#20930=ADVANCED_FACE ( 'NONE', ( #10268 ), #2659, .T. ) ;
#20945=FACE_OUTER_BOUND ( 'NONE', #44796, .T. ) ;
#20956=EDGE_LOOP ( 'NONE', ( #1036, #33053, #23614, #3164, #34600, #4518 ) ) ;
#20969=ORIENTED_EDGE ( 'NONE', *, *, #17079, .T. ) ;
#20978=ORIENTED_EDGE ( 'NONE', *, *, #28363, .F. ) ;
#20996=FACE_OUTER_BOUND ( 'NONE', #20956, .T. ) ;
#21005=EDGE_CURVE ( 'NONE', #42174, #28618, #37204, .T. ) ;
#21033=CYLINDRICAL_SURFACE ( 'NONE', #37124, 1.000000000000000888 ) ;
#21083=DIRECTION ( 'NONE',  ( -1.000000000000000000, 0.000000000000000000, 0.000000000000000000 ) ) ;
#21102=VECTOR ( 'NONE', #17228, 1000.000000000000000 ) ;
#21107=DIRECTION ( 'NONE',  ( -1.058954862565134068E-16, 0.6438296778008191223, -0.7651688349527137056 ) ) ;
#21131=DIRECTION ( 'NONE',  ( -1.058954862565134068E-16, 0.6438296778008191223, -0.7651688349527137056 ) ) ;
#21135=ORIENTED_EDGE ( 'NONE', *, *, #45318, .T. ) ;
#21166=CARTESIAN_POINT ( 'NONE',  ( -2.174186756557595869E-13, 469.9999999999994884, 0.000000000000000000 ) ) ;
#21201=VERTEX_POINT ( 'NONE', #7722 ) ;
#21218=CARTESIAN_POINT ( 'NONE',  ( 914.9999999999990905, 469.9999999999999432, 350.0000000000000000 ) ) ;
#21224=ORIENTED_EDGE ( 'NONE', *, *, #2348, .T. ) ;
#21253=DIRECTION ( 'NONE',  ( 1.258530456726092671E-16, -0.7651688349527167032, -0.6438296778008156807 ) ) ;
#21271=ORIENTED_EDGE ( 'NONE', *, *, #23244, .T. ) ;
#21286=DIRECTION ( 'NONE',  ( -1.000000000000000000, 0.000000000000000000, 0.000000000000000000 ) ) ;
#21303=ORIENTED_EDGE ( 'NONE', *, *, #31506, .F. ) ;
#21309=ORIENTED_EDGE ( 'NONE', *, *, #11465, .T. ) ;
#21311=CARTESIAN_POINT ( 'NONE',  ( 939.9999999999993179, -600.0000000000001137, 360.0000000000000000 ) ) ;
#21312=ORIENTED_EDGE ( 'NONE', *, *, #12270, .F. ) ;
#21370=ORIENTED_EDGE ( 'NONE', *, *, #10900, .F. ) ;
#21379=ORIENTED_EDGE ( 'NONE', *, *, #29470, .T. ) ;
#21398=CARTESIAN_POINT ( 'NONE',  ( 939.9999999999993179, 56.78581973499407809, 212.6378164459127618 ) ) ;
#21417=EDGE_LOOP ( 'NONE', ( #19892, #6815, #44311, #29828 ) ) ;
#21429=EDGE_LOOP ( 'NONE', ( #27612, #15670, #3022, #14219 ) ) ;
#21430=PRODUCT_CONTEXT ( 'NONE', #19885, 'mechanical' ) ;
#21442=CARTESIAN_POINT ( 'NONE',  ( 999.9999999999992042, 478.9999999999999432, 200.9999999999999432 ) ) ;
#21470=ORIENTED_EDGE ( 'NONE', *, *, #12270, .T. ) ;
#21478=EDGE_LOOP ( 'NONE', ( #18391, #34755, #43828 ) ) ;
#21483=EDGE_CURVE ( 'NONE', #1277, #14035, #15557, .T. ) ;
#21525=VERTEX_POINT ( 'NONE', #44174 ) ;
#21545=CARTESIAN_POINT ( 'NONE',  ( 998.9999999999992042, -600.0000000000001137, 360.0000000000000000 ) ) ;
#21546=CARTESIAN_POINT ( 'NONE',  ( 989.9999999999992042, -422.8782571739196783, 207.4246812887968190 ) ) ;
#21550=CARTESIAN_POINT ( 'NONE',  ( 914.9999999999992042, 74.99999999999984368, -360.0000000000000000 ) ) ;
#21591=EDGE_CURVE ( 'NONE', #6854, #28329, #4383, .T. ) ;
#21607=ORIENTED_EDGE ( 'NONE', *, *, #16099, .T. ) ;
#21617=DIRECTION ( 'NONE',  ( 0.000000000000000000, -0.6438296778008156807, 0.7651688349527167032 ) ) ;
#21670=CARTESIAN_POINT ( 'NONE',  ( 879.9999999999992042, 99.99999999999984368, 350.0000000000000000 ) ) ;
#21673=ORIENTED_EDGE ( 'NONE', *, *, #24578, .F. ) ;
#21704=VECTOR ( 'NONE', #6736, 1000.000000000000000 ) ;
#21720=AXIS2_PLACEMENT_3D ( 'NONE', #12819, #19984, #13517 ) ;
#21736=CIRCLE ( 'NONE', #1801, 8.000000000000007105 ) ;
#21757=AXIS2_PLACEMENT_3D ( 'NONE', #9184, #39551, #22583 ) ;
#21782=CARTESIAN_POINT ( 'NONE',  ( 914.9999999999992042, -426.1357934546398383, -350.0000000000000000 ) ) ;
#21784=ORIENTED_EDGE ( 'NONE', *, *, #41912, .F. ) ;
#21788=FACE_OUTER_BOUND ( 'NONE', #15199, .T. ) ;
#21860=EDGE_CURVE ( 'NONE', #17501, #21525, #9372, .T. ) ;
#21890=EDGE_LOOP ( 'NONE', ( #2042, #42325, #31254, #21673, #5681, #7976, #10460, #10950, #40637, #21379, #19612, #9152, #22102, #21135, #7865 ) ) ;
#21892=VECTOR ( 'NONE', #4468, 1000.000000000000000 ) ;
#21913=DIRECTION ( 'NONE',  ( 0.000000000000000000, 1.000000000000000000, 0.000000000000000000 ) ) ;
#21929=CIRCLE ( 'NONE', #7191, 7.999999999999896083 ) ;
#21950=ORIENTED_EDGE ( 'NONE', *, *, #5210, .F. ) ;
#21958=ORIENTED_EDGE ( 'NONE', *, *, #44243, .T. ) ;
#21990=CONICAL_SURFACE ( 'NONE', #27129, 8.024999999999948841, 0.7853981633963380560 ) ;
#22004=ORIENTED_EDGE ( 'NONE', *, *, #23244, .F. ) ;
#22013=LINE ( 'NONE', #21546, #27066 ) ;
#22015=CARTESIAN_POINT ( 'NONE',  ( 999.9999999999992042, -600.0000000000001137, -360.0000000000000000 ) ) ;
#22072=DIRECTION ( 'NONE',  ( -0.000000000000000000, -0.000000000000000000, 1.000000000000000000 ) ) ;
#22083=AXIS2_PLACEMENT_3D ( 'NONE', #44117, #44821, #2080 ) ;
#22088=LINE ( 'NONE', #3859, #29830 ) ;
#22102=ORIENTED_EDGE ( 'NONE', *, *, #35748, .F. ) ;
#22131=ORIENTED_EDGE ( 'NONE', *, *, #10900, .T. ) ;
#22169=EDGE_LOOP ( 'NONE', ( #1981, #41371, #36354, #7124 ) ) ;
#22184=EDGE_CURVE ( 'NONE', #15471, #6074, #9599, .T. ) ;
#22186=FACE_OUTER_BOUND ( 'NONE', #10555, .T. ) ;
#22232=LINE ( 'NONE', #35413, #29795 ) ;
#22251=LINE ( 'NONE', #24814, #32845 ) ;
#22263=ORIENTED_EDGE ( 'NONE', *, *, #30653, .T. ) ;
#22302=CARTESIAN_POINT ( 'NONE',  ( 999.9999999999992042, -599.0000000000001137, -359.0000000000000000 ) ) ;
#22332=CARTESIAN_POINT ( 'NONE',  ( 998.9999999999992042, 249.9999999999998863, -360.0000000000000000 ) ) ;
#22345=CARTESIAN_POINT ( 'NONE',  ( 879.9999999999992042, 99.99999999999984368, -360.0000000000000000 ) ) ;
#22378=AXIS2_PLACEMENT_3D ( 'NONE', #25311, #39424, #35948 ) ;
#22380=EDGE_LOOP ( 'NONE', ( #10678, #6936, #31238, #31362, #13577, #43835, #30123, #19668, #33749, #45544, #9777, #8372 ) ) ;
#22429=EDGE_CURVE ( 'NONE', #4120, #36456, #14439, .T. ) ;
#22452=ORIENTED_EDGE ( 'NONE', *, *, #35629, .T. ) ;
#22458=LINE ( 'NONE', #14879, #37071 ) ;
#22476=LINE ( 'NONE', #5161, #20326 ) ;
#22488=CIRCLE ( 'NONE', #26189, 8.024999999999948841 ) ;
#22498=AXIS2_PLACEMENT_3D ( 'NONE', #35723, #18196, #8026 ) ;
#22504=AXIS2_PLACEMENT_3D ( 'NONE', #23383, #43953, #12097 ) ;
#22534=VECTOR ( 'NONE', #43057, 1000.000000000000000 ) ;
#22542=CIRCLE ( 'NONE', #9270, 8.024999999999948841 ) ;
#22560=VECTOR ( 'NONE', #40492, 1000.000000000000000 ) ;
#22573=DIRECTION ( 'NONE',  ( 0.000000000000000000, -1.000000000000000000, 0.000000000000000000 ) ) ;
#22583=DIRECTION ( 'NONE',  ( 0.000000000000000000, -0.6438296778008192334, 0.7651688349527138167 ) ) ;
#22598=EDGE_LOOP ( 'NONE', ( #16079, #9718, #13032 ) ) ;
#22601=VECTOR ( 'NONE', #3624, 1000.000000000000114 ) ;
#22617=ORIENTED_EDGE ( 'NONE', *, *, #35689, .T. ) ;
#22626=EDGE_CURVE ( 'NONE', #9857, #12054, #22251, .T. ) ;
#22629=CIRCLE ( 'NONE', #6395, 7.999999999999896083 ) ;
#22644=FACE_OUTER_BOUND ( 'NONE', #22380, .T. ) ;
#22659=EDGE_CURVE ( 'NONE', #33885, #28618, #1247, .T. ) ;
#22679=ADVANCED_FACE ( 'NONE', ( #1462 ), #15349, .F. ) ;
#22707=CARTESIAN_POINT ( 'NONE',  ( 989.9999999999992042, -184.9457194955396631, -62.92409052808250891 ) ) ;
#22713=EDGE_CURVE ( 'NONE', #4120, #16303, #19035, .T. ) ;
#22718=DIRECTION ( 'NONE',  ( -0.000000000000000000, -0.000000000000000000, 1.000000000000000000 ) ) ;
#22719=VERTEX_POINT ( 'NONE', #19244 ) ;
#22731=EDGE_CURVE ( 'NONE', #29779, #3603, #13684, .T. ) ;
#22743=CARTESIAN_POINT ( 'NONE',  ( 989.9999999999992042, 240.0000000000001990, 201.9999999999999716 ) ) ;
#22847=LINE ( 'NONE', #5293, #39591 ) ;
#22848=FACE_BOUND ( 'NONE', #18600, .T. ) ;
#22849=PLANE ( 'NONE',  #26075 ) ;
#22864=CARTESIAN_POINT ( 'NONE',  ( 939.9999999999993179, 62.79977829742944095, 207.3621835540873235 ) ) ;
#22867=LINE ( 'NONE', #1844, #32416 ) ;
#22881=EDGE_CURVE ( 'NONE', #5961, #39395, #1908, .T. ) ;
#22885=VERTEX_POINT ( 'NONE', #26618 ) ;
#22899=CARTESIAN_POINT ( 'NONE',  ( 919.9999999999993179, 154.9999999999998863, -359.9749999999999659 ) ) ;
#22927=ORIENTED_EDGE ( 'NONE', *, *, #22626, .T. ) ;
#22933=ORIENTED_EDGE ( 'NONE', *, *, #27840, .F. ) ;
#22953=DIRECTION ( 'NONE',  ( 0.000000000000000000, -1.000000000000000000, -1.672022627447524993E-16 ) ) ;
#23019=ORIENTED_EDGE ( 'NONE', *, *, #41912, .T. ) ;
#23061=CARTESIAN_POINT ( 'NONE',  ( 939.9999999999992042, 74.99999999999984368, -350.0000000000000000 ) ) ;
#23062=DIRECTION ( 'NONE',  ( 0.000000000000000000, -0.6438296778008192334, 0.7651688349527138167 ) ) ;
#23081=VECTOR ( 'NONE', #36870, 1000.000000000000000 ) ;
#23153=CARTESIAN_POINT ( 'NONE',  ( 0.000000000000000000, 0.000000000000000000, 0.000000000000000000 ) ) ;
#23171=DIRECTION ( 'NONE',  ( 1.000000000000000000, 0.000000000000000000, 0.000000000000000000 ) ) ;
#23179=CARTESIAN_POINT ( 'NONE',  ( 187.1337867209877857, 62.85347435602256638, -357.4246812887967053 ) ) ;
#23199=CARTESIAN_POINT ( 'NONE',  ( 998.9999999999992042, -600.0000000000001137, -360.0000000000000000 ) ) ;
#23201=CYLINDRICAL_SURFACE ( 'NONE', #1854, 7.999999999999896083 ) ;
#23204=ORIENTED_EDGE ( 'NONE', *, *, #13049, .T. ) ;
#23241=VECTOR ( 'NONE', #40214, 1000.000000000000000 ) ;
#23244=EDGE_CURVE ( 'NONE', #35615, #27491, #13319, .T. ) ;
#23246=CARTESIAN_POINT ( 'NONE',  ( 927.9999999999993179, 219.9999999999998863, -359.9749999999999659 ) ) ;
#23254=CARTESIAN_POINT ( 'NONE',  ( 939.9999999999993179, -431.4567479753240491, -350.0000000000000000 ) ) ;
#23268=LINE ( 'NONE', #5485, #45369 ) ;
#23325=VECTOR ( 'NONE', #33255, 1000.000000000000000 ) ;
#23342=ORIENTED_EDGE ( 'NONE', *, *, #14859, .T. ) ;
#23344=VECTOR ( 'NONE', #14174, 1000.000000000000000 ) ;
#23350=VECTOR ( 'NONE', #37910, 1000.000000000000000 ) ;
#23353=VERTEX_POINT ( 'NONE', #34774 ) ;
#23356=LINE ( 'NONE', #21218, #23350 ) ;
#23383=CARTESIAN_POINT ( 'NONE',  ( 999.9999999999992042, -600.0000000000001137, -360.0000000000000000 ) ) ;
#23392=DIRECTION ( 'NONE',  ( 0.000000000000000000, 0.000000000000000000, 1.000000000000000000 ) ) ;
#23412=LINE ( 'NONE', #8884, #32204 ) ;
#23614=ORIENTED_EDGE ( 'NONE', *, *, #26674, .T. ) ;
#23627=DIRECTION ( 'NONE',  ( 0.000000000000000000, 0.000000000000000000, -1.000000000000000000 ) ) ;
#23641=DIRECTION ( 'NONE',  ( 0.000000000000000000, 0.000000000000000000, 1.000000000000000000 ) ) ;
#23645=CARTESIAN_POINT ( 'NONE',  ( 187.1337867209877857, -190.2822455671962985, -69.00746428064726956 ) ) ;
#23648=DIRECTION ( 'NONE',  ( 0.000000000000000000, 0.7517448203044204691, -0.6594541114781790059 ) ) ;
#23709=ORIENTED_EDGE ( 'NONE', *, *, #41497, .F. ) ;
#23728=ORIENTED_EDGE ( 'NONE', *, *, #13648, .T. ) ;
#23740=ORIENTED_EDGE ( 'NONE', *, *, #5490, .T. ) ;
#23746=VERTEX_POINT ( 'NONE', #3832 ) ;
#23759=CARTESIAN_POINT ( 'NONE',  ( 879.9999999999992042, 249.9999999999998295, 199.9999999999997442 ) ) ;
#23782=CARTESIAN_POINT ( 'NONE',  ( 999.9999999999992042, -599.0000000000001137, -360.0000000000000000 ) ) ;
#23795=EDGE_LOOP ( 'NONE', ( #2867, #14157, #4686, #7241 ) ) ;
#23798=LINE ( 'NONE', #2810, #11576 ) ;
#23839=EDGE_LOOP ( 'NONE', ( #21950, #28233, #26436, #19351, #15798, #31109, #25853 ) ) ;
#23857=FACE_OUTER_BOUND ( 'NONE', #21429, .T. ) ;
#23913=CARTESIAN_POINT ( 'NONE',  ( 989.9999999999992042, -418.3138125091626307, 201.9999999999998010 ) ) ;
#23936=DIRECTION ( 'NONE',  ( 1.000000000000000000, 0.000000000000000000, 0.000000000000000000 ) ) ;
#24001=AXIS2_PLACEMENT_3D ( 'NONE', #21166, #24382, #38272 ) ;
#24036=DIRECTION ( 'NONE',  ( 0.000000000000000000, -0.7651688349527138167, -0.6438296778008192334 ) ) ;
#24073=PLANE ( 'NONE',  #33017 ) ;
#24077=ORIENTED_EDGE ( 'NONE', *, *, #45318, .F. ) ;
#24082=ORIENTED_EDGE ( 'NONE', *, *, #35964, .T. ) ;
#24088=FACE_OUTER_BOUND ( 'NONE', #10927, .T. ) ;
#24100=EDGE_CURVE ( 'NONE', #33818, #4120, #32395, .T. ) ;
#24108=CARTESIAN_POINT ( 'NONE',  ( 999.9999999999992042, 479.5857864376268935, 359.5857864376268935 ) ) ;
#24179=DIRECTION ( 'NONE',  ( 0.000000000000000000, 0.000000000000000000, 1.000000000000000000 ) ) ;
#24195=ORIENTED_EDGE ( 'NONE', *, *, #5145, .F. ) ;
#24262=ORIENTED_EDGE ( 'NONE', *, *, #7816, .T. ) ;
#24308=ORIENTED_EDGE ( 'NONE', *, *, #11210, .T. ) ;
#24335=FACE_OUTER_BOUND ( 'NONE', #39346, .T. ) ;
#24382=DIRECTION ( 'NONE',  ( -4.625929269271485914E-16, 1.000000000000000000, 0.000000000000000000 ) ) ;
#24386=LINE ( 'NONE', #6403, #164 ) ;
#24409=CARTESIAN_POINT ( 'NONE',  ( 999.9999999999992042, 479.5857864376268935, 200.4142135623730496 ) ) ;
#24433=ORIENTED_EDGE ( 'NONE', *, *, #24100, .T. ) ;
#24451=DIRECTION ( 'NONE',  ( 0.000000000000000000, 0.000000000000000000, -1.000000000000000000 ) ) ;
#24472=VECTOR ( 'NONE', #8893, 1000.000000000000000 ) ;
#24503=DIRECTION ( 'NONE',  ( 0.000000000000000000, 0.000000000000000000, -1.000000000000000000 ) ) ;
#24517=CARTESIAN_POINT ( 'NONE',  ( 989.9999999999992042, 56.78581973499402835, 212.6378164459127049 ) ) ;
#24578=EDGE_CURVE ( 'NONE', #14210, #6074, #39763, .T. ) ;
#24598=ORIENTED_EDGE ( 'NONE', *, *, #15628, .T. ) ;
#24605=DIRECTION ( 'NONE',  ( -0.000000000000000000, -0.000000000000000000, 1.000000000000000000 ) ) ;
#24669=DIRECTION ( 'NONE',  ( 1.000000000000000000, 0.000000000000000000, 0.000000000000000000 ) ) ;
#24706=LINE ( 'NONE', #7626, #27917 ) ;
#24711=ADVANCED_FACE ( 'NONE', ( #5973 ), #9457, .T. ) ;
#24735=ADVANCED_FACE ( 'NONE', ( #30454 ), #19845, .F. ) ;
#24742=CARTESIAN_POINT ( 'NONE',  ( 999.9999999999992042, 249.9999999999998863, -360.0000000000000000 ) ) ;
#24790=CARTESIAN_POINT ( 'NONE',  ( 914.9999999999992042, 74.99999999999984368, 360.0000000000000000 ) ) ;
#24814=CARTESIAN_POINT ( 'NONE',  ( 1820.038553321469863, 47.45399382421944523, 201.9999999999999432 ) ) ;
#24815=LINE ( 'NONE', #32670, #35066 ) ;
#24882=AXIS2_PLACEMENT_3D ( 'NONE', #27603, #20668, #34759 ) ;
#24902=PLANE ( 'NONE',  #42565 ) ;
#24909=EDGE_LOOP ( 'NONE', ( #22927, #29885, #43919, #27343 ) ) ;
#24919=CYLINDRICAL_SURFACE ( 'NONE', #26220, 7.999999999999896083 ) ;
#24975=EDGE_CURVE ( 'NONE', #36456, #5823, #22847, .T. ) ;
#24998=ORIENTED_EDGE ( 'NONE', *, *, #11465, .F. ) ;
#25006=EDGE_LOOP ( 'NONE', ( #35962, #10457, #42737, #14816 ) ) ;
#25077=PLANE ( 'NONE',  #25478 ) ;
#25106=EDGE_CURVE ( 'NONE', #12726, #23746, #6450, .T. ) ;
#25124=DIRECTION ( 'NONE',  ( 1.000000000000000000, 0.000000000000000000, 0.000000000000000000 ) ) ;
#25154=ORIENTED_EDGE ( 'NONE', *, *, #34453, .T. ) ;
#25175=FACE_OUTER_BOUND ( 'NONE', #20347, .T. ) ;
#25239=FACE_BOUND ( 'NONE', #18273, .T. ) ;
#25244=CARTESIAN_POINT ( 'NONE',  ( 999.9999999999992042, -590.0000000000001137, -360.0000000000000000 ) ) ;
#25269=EDGE_LOOP ( 'NONE', ( #33034, #15970 ) ) ;
#25296=DIRECTION ( 'NONE',  ( 0.000000000000000000, 0.000000000000000000, -1.000000000000000000 ) ) ;
#25311=CARTESIAN_POINT ( 'NONE',  ( 919.9999999999993179, 219.9999999999998863, -360.0000000000000000 ) ) ;
#25360=LINE ( 'NONE', #43595, #12325 ) ;
#25366=VECTOR ( 'NONE', #35203, 1000.000000000000114 ) ;
#25389=VERTEX_POINT ( 'NONE', #21442 ) ;
#25423=DIRECTION ( 'NONE',  ( -1.000000000000000000, 0.000000000000000000, 0.000000000000000000 ) ) ;
#25427=PLANE ( 'NONE',  #42415 ) ;
#25459=AXIS2_PLACEMENT_3D ( 'NONE', #27359, #23648, #44924 ) ;
#25478=AXIS2_PLACEMENT_3D ( 'NONE', #7541, #21617, #35699 ) ;
#25534=ORIENTED_EDGE ( 'NONE', *, *, #41383, .T. ) ;
#25550=DIRECTION ( 'NONE',  ( 0.000000000000000000, 1.000000000000000000, 0.000000000000000000 ) ) ;
#25603=CARTESIAN_POINT ( 'NONE',  ( 919.9999999999993179, 154.9999999999998863, 350.0000000000000000 ) ) ;
#25612=LINE ( 'NONE', #23645, #8666 ) ;
#25667=DIRECTION ( 'NONE',  ( 0.000000000000000000, -0.7651688349527138167, -0.6438296778008192334 ) ) ;
#25680=VECTOR ( 'NONE', #16888, 1000.000000000000000 ) ;
#25689=ORIENTED_EDGE ( 'NONE', *, *, #22659, .T. ) ;
#25745=ORIENTED_EDGE ( 'NONE', *, *, #29246, .F. ) ;
#25818=DIRECTION ( 'NONE',  ( 1.000000000000000000, 0.000000000000000000, 0.000000000000000000 ) ) ;
#25839=EDGE_CURVE ( 'NONE', #19255, #8608, #15218, .T. ) ;
#25842=LINE ( 'NONE', #24517, #37345 ) ;
#25853=ORIENTED_EDGE ( 'NONE', *, *, #3316, .F. ) ;
#25903=SHAPE_REPRESENTATION_RELATIONSHIP ( 'NONE' , 'NONE' ,  #27662, #17201 ) ;
#25943=LINE ( 'NONE', #43954, #40269 ) ;
#25966=CARTESIAN_POINT ( 'NONE',  ( 939.9999999999993179, -590.0000000000001137, -360.0000000000000000 ) ) ;
#25980=VECTOR ( 'NONE', #25818, 1000.000000000000000 ) ;
#25996=EDGE_LOOP ( 'NONE', ( #44409, #25534, #28980, #44363 ) ) ;
#26075=AXIS2_PLACEMENT_3D ( 'NONE', #36942, #26543, #23062 ) ;
#26116=EDGE_CURVE ( 'NONE', #28819, #1155, #36892, .T. ) ;
#26145=CARTESIAN_POINT ( 'NONE',  ( 879.9999999999990905, 479.9999999999998863, 199.9999999999999716 ) ) ;
#26159=EDGE_CURVE ( 'NONE', #15686, #8608, #16325, .T. ) ;
#26186=CARTESIAN_POINT ( 'NONE',  ( 989.9999999999992042, 249.9999999999998863, 350.0000000000000000 ) ) ;
#26189=AXIS2_PLACEMENT_3D ( 'NONE', #42540, #4208, #15286 ) ;
#26220=AXIS2_PLACEMENT_3D ( 'NONE', #4154, #42482, #39493 ) ;
#26279=DIRECTION ( 'NONE',  ( 1.000000000000000000, 0.000000000000000000, 0.000000000000000000 ) ) ;
#26292=AXIS2_PLACEMENT_3D ( 'NONE', #45365, #10027, #7015 ) ;
#26304=FACE_OUTER_BOUND ( 'NONE', #39574, .T. ) ;
#26341=CARTESIAN_POINT ( 'NONE',  ( 939.9999999999992042, 240.0000000000000568, 210.0000000000000000 ) ) ;
#26364=VERTEX_POINT ( 'NONE', #2927 ) ;
#26404=CARTESIAN_POINT ( 'NONE',  ( 939.9999999999992042, 74.99999999999984368, -360.0000000000000000 ) ) ;
#26406=DIRECTION ( 'NONE',  ( -1.084653538143406060E-16, 0.6594541114781790059, 0.7517448203044204691 ) ) ;
#26418=DIRECTION ( 'NONE',  ( -0.000000000000000000, -0.000000000000000000, 1.000000000000000000 ) ) ;
#26435=FACE_OUTER_BOUND ( 'NONE', #23795, .T. ) ;
#26436=ORIENTED_EDGE ( 'NONE', *, *, #44243, .F. ) ;
#26444=CARTESIAN_POINT ( 'NONE',  ( 879.9999999999992042, 469.9999999999998863, -360.0000000000000000 ) ) ;
#26450=CARTESIAN_POINT ( 'NONE',  ( 989.9999999999992042, 50.81038600091411439, 210.0000000000000000 ) ) ;
#26539=ORIENTED_EDGE ( 'NONE', *, *, #21860, .F. ) ;
#26541=DIRECTION ( 'NONE',  ( 0.000000000000000000, 0.000000000000000000, -1.000000000000000000 ) ) ;
#26543=DIRECTION ( 'NONE',  ( 0.000000000000000000, -0.7651688349527138167, -0.6438296778008192334 ) ) ;
#26558=DIRECTION ( 'NONE',  ( 1.337618101958019798E-16, -1.000000000000000000, 0.000000000000000000 ) ) ;
#26559=( NAMED_UNIT ( * ) PLANE_ANGLE_UNIT ( ) SI_UNIT ( $, .RADIAN. ) );
#26611=EDGE_CURVE ( 'NONE', #8154, #15790, #19709, .T. ) ;
#26618=CARTESIAN_POINT ( 'NONE',  ( 989.9999999999992042, -185.0721577059061929, -75.19946970736501157 ) ) ;
#26628=EDGE_CURVE ( 'NONE', #15565, #5169, #11615, .T. ) ;
#26647=CARTESIAN_POINT ( 'NONE',  ( 939.9999999999993179, -600.0000000000001137, -360.0000000000000000 ) ) ;
#26657=DIRECTION ( 'NONE',  ( 0.000000000000000000, -1.000000000000000000, 0.000000000000000000 ) ) ;
#26661=EDGE_CURVE ( 'NONE', #27491, #14210, #44034, .T. ) ;
#26662=CARTESIAN_POINT ( 'NONE',  ( 879.9999999999990905, 479.9999999999998863, 360.0000000000000000 ) ) ;
#26674=EDGE_CURVE ( 'NONE', #11542, #13265, #7765, .T. ) ;
#26679=DIRECTION ( 'NONE',  ( -1.337618101958019798E-16, 1.000000000000000000, 1.672022627447524747E-16 ) ) ;
#26828=CARTESIAN_POINT ( 'NONE',  ( 927.9999999999992042, 219.9999999999998863, -350.0000000000000000 ) ) ;
#26858=AXIS2_PLACEMENT_3D ( 'NONE', #23153, #34241, #6075 ) ;
#26861=ORIENTED_EDGE ( 'NONE', *, *, #6037, .T. ) ;
#26867=DIRECTION ( 'NONE',  ( -0.000000000000000000, -0.000000000000000000, 1.000000000000000000 ) ) ;
#26921=VECTOR ( 'NONE', #37308, 1000.000000000000000 ) ;
#26934=LINE ( 'NONE', #40375, #28433 ) ;
#26948=LINE ( 'NONE', #12865, #14548 ) ;
#26961=VECTOR ( 'NONE', #21131, 1000.000000000000114 ) ;
#26980=ORIENTED_EDGE ( 'NONE', *, *, #5145, .T. ) ;
#27025=CARTESIAN_POINT ( 'NONE',  ( 879.9999999999990905, 479.9999999999998863, 199.9999999999999716 ) ) ;
#27059=ORIENTED_EDGE ( 'NONE', *, *, #11177, .T. ) ;
#27064=ORIENTED_EDGE ( 'NONE', *, *, #25106, .T. ) ;
#27066=VECTOR ( 'NONE', #4001, 1000.000000000000000 ) ;
#27073=VERTEX_POINT ( 'NONE', #19497 ) ;
#27088=CARTESIAN_POINT ( 'NONE',  ( 919.9999999999993179, 219.9999999999998863, -350.0000000000000000 ) ) ;
#27099=ORIENTED_EDGE ( 'NONE', *, *, #36083, .T. ) ;
#27122=EDGE_LOOP ( 'NONE', ( #12009, #7117, #4170, #17408 ) ) ;
#27129=AXIS2_PLACEMENT_3D ( 'NONE', #288, #42783, #11145 ) ;
#27135=CARTESIAN_POINT ( 'NONE',  ( 999.9999999999992042, 249.5857864376267798, 200.4142135623730496 ) ) ;
#27154=PLANE ( 'NONE',  #36522 ) ;
#27164=EDGE_LOOP ( 'NONE', ( #7051, #37387, #6765, #35792 ) ) ;
#27209=EDGE_CURVE ( 'NONE', #25389, #28026, #19967, .T. ) ;
#27221=ORIENTED_EDGE ( 'NONE', *, *, #35972, .T. ) ;
#27305=PLANE ( 'NONE',  #43113 ) ;
#27310=EDGE_CURVE ( 'NONE', #9857, #41889, #8679, .T. ) ;
#27336=VERTEX_POINT ( 'NONE', #44913 ) ;
#27343=ORIENTED_EDGE ( 'NONE', *, *, #14519, .F. ) ;
#27356=CARTESIAN_POINT ( 'NONE',  ( 999.9999999999992042, 478.9999999999999432, 359.0000000000000000 ) ) ;
#27359=CARTESIAN_POINT ( 'NONE',  ( 187.1337867209877857, 56.78581973499402835, 212.6378164459127049 ) ) ;
#27371=CARTESIAN_POINT ( 'NONE',  ( 999.9999999999992042, -590.0000000000001137, -360.0000000000000000 ) ) ;
#27411=EDGE_CURVE ( 'NONE', #8915, #13265, #13271, .T. ) ;
#27419=AXIS2_PLACEMENT_3D ( 'NONE', #32594, #4204, #25423 ) ;
#27448=ORIENTED_EDGE ( 'NONE', *, *, #42479, .T. ) ;
#27469=FACE_OUTER_BOUND ( 'NONE', #19830, .T. ) ;
#27490=DIRECTION ( 'NONE',  ( 0.000000000000000000, -0.6594541114781782287, -0.7517448203044211352 ) ) ;
#27491=VERTEX_POINT ( 'NONE', #6560 ) ;
#27501=VECTOR ( 'NONE', #23641, 1000.000000000000000 ) ;
#27537=ORIENTED_EDGE ( 'NONE', *, *, #25839, .T. ) ;
#27559=ADVANCED_FACE ( 'NONE', ( #7021, #27571, #13954, #44682 ), #10032, .F. ) ;
#27571=FACE_BOUND ( 'NONE', #9419, .T. ) ;
#27603=CARTESIAN_POINT ( 'NONE',  ( 919.9999999999993179, 154.9999999999998863, -360.0000000000000000 ) ) ;
#27612=ORIENTED_EDGE ( 'NONE', *, *, #15628, .F. ) ;
#27615=AXIS2_PLACEMENT_3D ( 'NONE', #5501, #44310, #19595 ) ;
#27621=AXIS2_PLACEMENT_3D ( 'NONE', #13289, #41926, #44931 ) ;
#27627=CARTESIAN_POINT ( 'NONE',  ( 911.9749999999993406, 154.9999999999998863, -360.0000000000000000 ) ) ;
#27633=CLOSED_SHELL ( 'NONE', ( #3506, #10045, #35110, #32783, #6879, #13381, #34577, #12232, #27559, #14321, #2385, #2354, #36068, #36030, #41386, #44738, #30909, #37685, #44671, #9776, #7730, #24735, #17674, #17623, #22679, #13956, #13961, #30950, #29228, #17846, #38218, #27895, #43513, #32908, #6406, #12194, #30365, #4064, #33726, #12805, #3130, #44965, #24711, #40916, #19018, #992, #7773, #19347, #11135, #35440, #13666, #18504, #30925, #19876, #40501, #20930, #37996, #28831, #1539, #34339 ) ) ;
#27648=VECTOR ( 'NONE', #3866, 1000.000000000000000 ) ;
#27649=( BOUNDED_CURVE ( )  B_SPLINE_CURVE ( 3, ( #21545, #982, #7697, #43255 ),
 .UNSPECIFIED., .F., .T. ) 
 B_SPLINE_CURVE_WITH_KNOTS ( ( 4, 4 ),
 ( 3.141592653589793116, 4.712388980384689674 ),
 .UNSPECIFIED. ) 
 CURVE ( )  GEOMETRIC_REPRESENTATION_ITEM ( )  RATIONAL_B_SPLINE_CURVE ( ( 1.000000000000000000, 0.8047378541243649375, 0.8047378541243649375, 1.000000000000000000 ) ) 
 REPRESENTATION_ITEM ( '' )  );
#27662=SHAPE_REPRESENTATION ( 'MirrorHeavy Cast Iron Table Bed Base', ( #26858 ), #9809 ) ;
#27704=CARTESIAN_POINT ( 'NONE',  ( 879.9999999999990905, 479.9999999999998863, 360.0000000000000000 ) ) ;
#27727=CARTESIAN_POINT ( 'NONE',  ( 187.1337867209877857, -428.4497686941065808, -352.6378164459125060 ) ) ;
#27757=LINE ( 'NONE', #34910, #4763 ) ;
#27820=FACE_OUTER_BOUND ( 'NONE', #33311, .T. ) ;
#27840=EDGE_CURVE ( 'NONE', #20535, #5169, #22232, .T. ) ;
#27846=ORIENTED_EDGE ( 'NONE', *, *, #7195, .T. ) ;
#27871=CARTESIAN_POINT ( 'NONE',  ( 999.9999999999992042, -599.0000000000001137, 359.0000000000000000 ) ) ;
#27895=ADVANCED_FACE ( 'NONE', ( #21788 ), #3783, .T. ) ;
#27917=VECTOR ( 'NONE', #42727, 1000.000000000000000 ) ;
#27922=FACE_BOUND ( 'NONE', #25269, .T. ) ;
#27925=VERTEX_POINT ( 'NONE', #15095 ) ;
#27948=ORIENTED_EDGE ( 'NONE', *, *, #42431, .T. ) ;
#27969=ORIENTED_EDGE ( 'NONE', *, *, #31676, .F. ) ;
#28026=VERTEX_POINT ( 'NONE', #28953 ) ;
#28029=DIRECTION ( 'NONE',  ( 1.000000000000000000, 1.644774851296528363E-16, 0.000000000000000000 ) ) ;
#28083=CARTESIAN_POINT ( 'NONE',  ( 989.9999999999992042, 62.85347435602256638, -357.4246812887967053 ) ) ;
#28101=DIRECTION ( 'NONE',  ( -1.000000000000000000, 0.000000000000000000, 0.000000000000000000 ) ) ;
#28142=CARTESIAN_POINT ( 'NONE',  ( 989.9999999999992042, -428.4497686941065808, -352.6378164459125060 ) ) ;
#28233=ORIENTED_EDGE ( 'NONE', *, *, #31749, .F. ) ;
#28243=FACE_BOUND ( 'NONE', #40912, .T. ) ;
#28329=VERTEX_POINT ( 'NONE', #8838 ) ;
#28334=VERTEX_POINT ( 'NONE', #1444 ) ;
#28358=DIRECTION ( 'NONE',  ( 0.000000000000000000, 0.000000000000000000, -1.000000000000000000 ) ) ;
#28362=DIRECTION ( 'NONE',  ( 0.7071067811857625340, 0.000000000000000000, -0.7071067811873326114 ) ) ;
#28363=EDGE_CURVE ( 'NONE', #15194, #20750, #4708, .T. ) ;
#28366=LINE ( 'NONE', #42237, #28971 ) ;
#28412=CIRCLE ( 'NONE', #22498, 7.999999999999896083 ) ;
#28433=VECTOR ( 'NONE', #9396, 1000.000000000000114 ) ;
#28436=CYLINDRICAL_SURFACE ( 'NONE', #27419, 24.99999999999991118 ) ;
#28451=CARTESIAN_POINT ( 'NONE',  ( 939.9999999999993179, -600.0000000000001137, -350.0000000000000000 ) ) ;
#28491=DIRECTION ( 'NONE',  ( 1.000000000000000000, 0.000000000000000000, 0.000000000000000000 ) ) ;
#28492=ORIENTED_EDGE ( 'NONE', *, *, #39309, .T. ) ;
#28504=CARTESIAN_POINT ( 'NONE',  ( 998.9999999999992042, 249.9999999999998863, 359.0000000000000000 ) ) ;
#28506=VECTOR ( 'NONE', #40025, 1000.000000000000000 ) ;
#28573=FACE_OUTER_BOUND ( 'NONE', #21417, .T. ) ;
#28610=CARTESIAN_POINT ( 'NONE',  ( 187.1337867209877857, -416.7569064942979935, 212.5753187112033231 ) ) ;
#28614=DIRECTION ( 'NONE',  ( 0.000000000000000000, 0.000000000000000000, -1.000000000000000000 ) ) ;
#28618=VERTEX_POINT ( 'NONE', #44080 ) ;
#28639=EDGE_CURVE ( 'NONE', #9195, #22885, #44541, .T. ) ;
#28664=CARTESIAN_POINT ( 'NONE',  ( 998.9999999999992042, 249.9999999999998863, 200.9999999999999432 ) ) ;
#28751=DIRECTION ( 'NONE',  ( -1.000000000000000000, -4.625929269271485914E-16, -0.000000000000000000 ) ) ;
#28770=VERTEX_POINT ( 'NONE', #40625 ) ;
#28813=ORIENTED_EDGE ( 'NONE', *, *, #13974, .F. ) ;
#28819=VERTEX_POINT ( 'NONE', #33911 ) ;
#28831=ADVANCED_FACE ( 'NONE', ( #26304 ), #11997, .T. ) ;
#28833=ORIENTED_EDGE ( 'NONE', *, *, #40526, .F. ) ;
#28835=CARTESIAN_POINT ( 'NONE',  ( 939.9999999999993179, -600.0000000000001137, -360.0000000000000000 ) ) ;
#28953=CARTESIAN_POINT ( 'NONE',  ( 999.9999999999992042, 248.9999999999998863, 200.9999999999999432 ) ) ;
#28971=VECTOR ( 'NONE', #21913, 1000.000000000000000 ) ;
#28977=LINE ( 'NONE', #7729, #22534 ) ;
#28980=ORIENTED_EDGE ( 'NONE', *, *, #22881, .F. ) ;
#29008=DIRECTION ( 'NONE',  ( 0.000000000000000000, 0.000000000000000000, 1.000000000000000000 ) ) ;
#29067=LINE ( 'NONE', #19128, #44772 ) ;
#29120=ORIENTED_EDGE ( 'NONE', *, *, #27209, .F. ) ;
#29177=VERTEX_POINT ( 'NONE', #29327 ) ;
#29228=ADVANCED_FACE ( 'NONE', ( #32778 ), #4380, .T. ) ;
#29243=AXIS2_PLACEMENT_3D ( 'NONE', #31030, #23627, #31259 ) ;
#29246=EDGE_CURVE ( 'NONE', #33818, #19659, #18470, .T. ) ;
#29280=AXIS2_PLACEMENT_3D ( 'NONE', #39671, #11024, #39204 ) ;
#29327=CARTESIAN_POINT ( 'NONE',  ( 999.9999999999992042, 478.9999999999999432, 359.0000000000000000 ) ) ;
#29412=VECTOR ( 'NONE', #30777, 1000.000000000000000 ) ;
#29458=FACE_OUTER_BOUND ( 'NONE', #40073, .T. ) ;
#29470=EDGE_CURVE ( 'NONE', #33885, #577, #23268, .T. ) ;
#29522=CARTESIAN_POINT ( 'NONE',  ( 914.9999999999992042, 99.99999999999984368, 350.0000000000000000 ) ) ;
#29589=PLANE ( 'NONE',  #4391 ) ;
#29626=DIRECTION ( 'NONE',  ( 0.000000000000000000, 1.000000000000000000, 0.000000000000000000 ) ) ;
#29695=EDGE_CURVE ( 'NONE', #23353, #15565, #17507, .T. ) ;
#29699=FACE_OUTER_BOUND ( 'NONE', #8663, .T. ) ;
#29706=DIRECTION ( 'NONE',  ( 1.000000000000000000, 0.000000000000000000, 0.000000000000000000 ) ) ;
#29742=EDGE_LOOP ( 'NONE', ( #18084, #38429, #39218, #20846 ) ) ;
#29750=ORIENTED_EDGE ( 'NONE', *, *, #19370, .F. ) ;
#29779=VERTEX_POINT ( 'NONE', #41989 ) ;
#29785=DIRECTION ( 'NONE',  ( 1.000000000000000000, 0.000000000000000000, 0.000000000000000000 ) ) ;
#29795=VECTOR ( 'NONE', #32648, 1000.000000000000000 ) ;
#29828=ORIENTED_EDGE ( 'NONE', *, *, #34562, .T. ) ;
#29830=VECTOR ( 'NONE', #36178, 1000.000000000000000 ) ;
#29846=ORIENTED_EDGE ( 'NONE', *, *, #34562, .F. ) ;
#29865=CARTESIAN_POINT ( 'NONE',  ( 1820.038553321469863, -407.8586036264140375, 201.9999999999998863 ) ) ;
#29869=CARTESIAN_POINT ( 'NONE',  ( 998.9999999999992042, 249.9999999999998863, -360.0000000000000000 ) ) ;
#29885=ORIENTED_EDGE ( 'NONE', *, *, #31423, .F. ) ;
#29943=ORIENTED_EDGE ( 'NONE', *, *, #42215, .T. ) ;
#29984=AXIS2_PLACEMENT_3D ( 'NONE', #44436, #1940, #23171 ) ;
#29989=ORIENTED_EDGE ( 'NONE', *, *, #12563, .T. ) ;
#30109=EDGE_CURVE ( 'NONE', #1931, #15194, #10799, .T. ) ;
#30123=ORIENTED_EDGE ( 'NONE', *, *, #24975, .T. ) ;
#30286=CARTESIAN_POINT ( 'NONE',  ( 939.9999999999993179, -590.0000000000001137, -350.0000000000000000 ) ) ;
#30300=EDGE_CURVE ( 'NONE', #1931, #12197, #28412, .T. ) ;
#30312=DIRECTION ( 'NONE',  ( -0.000000000000000000, -0.000000000000000000, 1.000000000000000000 ) ) ;
#30313=DIRECTION ( 'NONE',  ( -1.000000000000000000, 0.000000000000000000, 0.000000000000000000 ) ) ;
#30349=DIRECTION ( 'NONE',  ( 0.000000000000000000, -1.000000000000000000, 0.000000000000000000 ) ) ;
#30365=ADVANCED_FACE ( 'NONE', ( #29699 ), #23201, .F. ) ;
#30417=CARTESIAN_POINT ( 'NONE',  ( 914.9999999999992042, 99.99999999999984368, -360.0000000000000000 ) ) ;
#30454=FACE_OUTER_BOUND ( 'NONE', #14635, .T. ) ;
#30461=AXIS2_PLACEMENT_3D ( 'NONE', #30585, #12369, #31043 ) ;
#30506=VERTEX_POINT ( 'NONE', #34066 ) ;
#30512=AXIS2_PLACEMENT_3D ( 'NONE', #4176, #7402, #35798 ) ;
#30572=ORIENTED_EDGE ( 'NONE', *, *, #37418, .T. ) ;
#30576=EDGE_LOOP ( 'NONE', ( #40064, #40523 ) ) ;
#30585=CARTESIAN_POINT ( 'NONE',  ( 919.9999999999993179, 219.9999999999998863, 360.0000000000000000 ) ) ;
#30610=FACE_OUTER_BOUND ( 'NONE', #8562, .T. ) ;
#30621=EDGE_LOOP ( 'NONE', ( #37212, #41657, #8673 ) ) ;
#30623=AXIS2_PLACEMENT_3D ( 'NONE', #20445, #31062, #13522 ) ;
#30653=EDGE_CURVE ( 'NONE', #5854, #40626, #13981, .T. ) ;
#30658=VECTOR ( 'NONE', #5610, 1000.000000000000000 ) ;
#30736=ORIENTED_EDGE ( 'NONE', *, *, #3230, .T. ) ;
#30777=DIRECTION ( 'NONE',  ( 0.000000000000000000, 0.000000000000000000, 1.000000000000000000 ) ) ;
#30828=CARTESIAN_POINT ( 'NONE',  ( 998.9999999999992042, 479.9999999999999432, 360.0000000000000000 ) ) ;
#30855=VECTOR ( 'NONE', #34661, 1000.000000000000000 ) ;
#30862=EDGE_LOOP ( 'NONE', ( #38791, #25689, #19111, #40582 ) ) ;
#30868=CARTESIAN_POINT ( 'NONE',  ( 919.9999999999993179, 219.9999999999998863, 360.0000000000000000 ) ) ;
#30875=CARTESIAN_POINT ( 'NONE',  ( 939.9999999999992042, 47.45399382421949497, 201.9999999999999432 ) ) ;
#30883=ORIENTED_EDGE ( 'NONE', *, *, #43119, .T. ) ;
#30909=ADVANCED_FACE ( 'NONE', ( #41466 ), #16762, .T. ) ;
#30925=ADVANCED_FACE ( 'NONE', ( #30610 ), #27154, .F. ) ;
#30950=ADVANCED_FACE ( 'NONE', ( #3113 ), #16985, .F. ) ;
#31027=ORIENTED_EDGE ( 'NONE', *, *, #37723, .F. ) ;
#31030=CARTESIAN_POINT ( 'NONE',  ( 919.9999999999993179, 219.9999999999998863, -360.0000000000000000 ) ) ;
#31043=DIRECTION ( 'NONE',  ( 1.000000000000000000, 0.000000000000000000, 0.000000000000000000 ) ) ;
#31046=CARTESIAN_POINT ( 'NONE',  ( 989.9999999999992042, 56.73212367640085318, -362.5753187112032379 ) ) ;
#31062=DIRECTION ( 'NONE',  ( 0.000000000000000000, 0.000000000000000000, 1.000000000000000000 ) ) ;
#31093=PLANE ( 'NONE',  #24001 ) ;
#31097=DIRECTION ( 'NONE',  ( -0.7071067811857625340, -8.659560562345319848E-17, -0.7071067811873326114 ) ) ;
#31109=ORIENTED_EDGE ( 'NONE', *, *, #22429, .F. ) ;
#31138=VECTOR ( 'NONE', #10777, 1000.000000000000000 ) ;
#31160=EDGE_CURVE ( 'NONE', #8154, #41883, #24815, .T. ) ;
#31220=PLANE ( 'NONE',  #15797 ) ;
#31238=ORIENTED_EDGE ( 'NONE', *, *, #30653, .F. ) ;
#31254=ORIENTED_EDGE ( 'NONE', *, *, #22184, .T. ) ;
#31259=DIRECTION ( 'NONE',  ( 1.000000000000000000, 0.000000000000000000, 0.000000000000000000 ) ) ;
#31307=ORIENTED_EDGE ( 'NONE', *, *, #39390, .F. ) ;
#31324=LINE ( 'NONE', #27627, #10009 ) ;
#31329=CARTESIAN_POINT ( 'NONE',  ( 939.9999999999992042, 74.99999999999984368, -360.0000000000000000 ) ) ;
#31332=AXIS2_PLACEMENT_3D ( 'NONE', #41567, #24451, #16867 ) ;
#31362=ORIENTED_EDGE ( 'NONE', *, *, #3268, .T. ) ;
#31364=AXIS2_PLACEMENT_3D ( 'NONE', #24742, #42757, #38860 ) ;
#31382=DIRECTION ( 'NONE',  ( 0.000000000000000000, -1.000000000000000000, 0.000000000000000000 ) ) ;
#31423=EDGE_CURVE ( 'NONE', #43869, #12054, #28977, .T. ) ;
#31434=VECTOR ( 'NONE', #39649, 1000.000000000000000 ) ;
#31480=VERTEX_POINT ( 'NONE', #22707 ) ;
#31499=CARTESIAN_POINT ( 'NONE',  ( 989.9999999999992042, 469.9999999999999432, -360.0000000000000000 ) ) ;
#31500=ORIENTED_EDGE ( 'NONE', *, *, #3230, .F. ) ;
#31506=EDGE_CURVE ( 'NONE', #6890, #12560, #11870, .T. ) ;
#31510=AXIS2_PLACEMENT_3D ( 'NONE', #42695, #35069, #2982 ) ;
#31550=AXIS2_PLACEMENT_3D ( 'NONE', #27727, #27490, #9717 ) ;
#31568=CARTESIAN_POINT ( 'NONE',  ( 939.9999999999993179, -179.7356316342496712, -69.11609595480024382 ) ) ;
#31625=CYLINDRICAL_SURFACE ( 'NONE', #31332, 7.999999999999896083 ) ;
#31643=DIRECTION ( 'NONE',  ( 0.000000000000000000, 0.000000000000000000, -1.000000000000000000 ) ) ;
#31676=EDGE_CURVE ( 'NONE', #17002, #28334, #25943, .T. ) ;
#31699=ORIENTED_EDGE ( 'NONE', *, *, #6400, .T. ) ;
#31718=DIRECTION ( 'NONE',  ( 0.000000000000000000, 1.000000000000000000, 0.000000000000000000 ) ) ;
#31749=EDGE_CURVE ( 'NONE', #43930, #11422, #22476, .T. ) ;
#31758=EDGE_CURVE ( 'NONE', #22719, #16202, #44181, .T. ) ;
#31768=ORIENTED_EDGE ( 'NONE', *, *, #12563, .F. ) ;
#31917=FACE_OUTER_BOUND ( 'NONE', #9573, .T. ) ;
#31964=VECTOR ( 'NONE', #14208, 1000.000000000000000 ) ;
#31968=ORIENTED_EDGE ( 'NONE', *, *, #41885, .T. ) ;
#32012=DIRECTION ( 'NONE',  ( 0.000000000000000000, 0.000000000000000000, -1.000000000000000000 ) ) ;
#32042=ORIENTED_EDGE ( 'NONE', *, *, #33687, .F. ) ;
#32055=VECTOR ( 'NONE', #15288, 1000.000000000000000 ) ;
#32062=DIRECTION ( 'NONE',  ( 0.000000000000000000, -0.6594541114781790059, -0.7517448203044204691 ) ) ;
#32063=PLANE ( 'NONE',  #43691 ) ;
#32187=FACE_OUTER_BOUND ( 'NONE', #18498, .T. ) ;
#32188=ORIENTED_EDGE ( 'NONE', *, *, #20717, .T. ) ;
#32204=VECTOR ( 'NONE', #16043, 1000.000000000000000 ) ;
#32275=EDGE_CURVE ( 'NONE', #5448, #39395, #25842, .T. ) ;
#32297=EDGE_CURVE ( 'NONE', #31480, #41889, #36239, .T. ) ;
#32309=FACE_BOUND ( 'NONE', #30576, .T. ) ;
#32373=PLANE ( 'NONE',  #38470 ) ;
#32395=( BOUNDED_CURVE ( )  B_SPLINE_CURVE ( 3, ( #19059, #36373, #1697, #37273 ),
 .UNSPECIFIED., .F., .T. ) 
 B_SPLINE_CURVE_WITH_KNOTS ( ( 4, 4 ),
 ( 1.570796326794896558, 3.141592653589793116 ),
 .UNSPECIFIED. ) 
 CURVE ( )  GEOMETRIC_REPRESENTATION_ITEM ( )  RATIONAL_B_SPLINE_CURVE ( ( 1.000000000000000000, 0.8047378541243649375, 0.8047378541243649375, 1.000000000000000000 ) ) 
 REPRESENTATION_ITEM ( '' )  );
#32416=VECTOR ( 'NONE', #13179, 1000.000000000000000 ) ;
#32485=FACE_OUTER_BOUND ( 'NONE', #12888, .T. ) ;
#32507=ORIENTED_EDGE ( 'NONE', *, *, #6355, .F. ) ;
#32533=DIRECTION ( 'NONE',  ( 0.7071067811857625340, 0.000000000000000000, -0.7071067811873326114 ) ) ;
#32537=ORIENTED_EDGE ( 'NONE', *, *, #22626, .F. ) ;
#32549=CARTESIAN_POINT ( 'NONE',  ( 999.9999999999992042, -600.0000000000001137, -359.0000000000000000 ) ) ;
#32592=LINE ( 'NONE', #18512, #32728 ) ;
#32594=CARTESIAN_POINT ( 'NONE',  ( 914.9999999999992042, 74.99999999999984368, -360.0000000000000000 ) ) ;
#32648=DIRECTION ( 'NONE',  ( 0.000000000000000000, 0.000000000000000000, -1.000000000000000000 ) ) ;
#32666=VECTOR ( 'NONE', #13844, 1000.000000000000227 ) ;
#32670=CARTESIAN_POINT ( 'NONE',  ( 911.9999999999993179, 154.9999999999998863, -360.0000000000000000 ) ) ;
#32724=CARTESIAN_POINT ( 'NONE',  ( 927.9999999999992042, 219.9999999999998863, -360.0000000000000000 ) ) ;
#32728=VECTOR ( 'NONE', #3095, 1000.000000000000000 ) ;
#32778=FACE_OUTER_BOUND ( 'NONE', #41213, .T. ) ;
#32783=ADVANCED_FACE ( 'NONE', ( #41993 ), #41776, .F. ) ;
#32845=VECTOR ( 'NONE', #38934, 1000.000000000000000 ) ;
#32860=VECTOR ( 'NONE', #38129, 1000.000000000000000 ) ;
#32907=EDGE_CURVE ( 'NONE', #10930, #25389, #37770, .T. ) ;
#32908=ADVANCED_FACE ( 'NONE', ( #17264, #38513, #20945 ), #35042, .T. ) ;
#32922=ORIENTED_EDGE ( 'NONE', *, *, #36821, .T. ) ;
#32942=CARTESIAN_POINT ( 'NONE',  ( 927.9999999999992042, 154.9999999999998863, -350.0000000000000000 ) ) ;
#33017=AXIS2_PLACEMENT_3D ( 'NONE', #37951, #17395, #21083 ) ;
#33027=CARTESIAN_POINT ( 'NONE',  ( 989.9999999999992042, 62.85347435602256638, -357.4246812887967053 ) ) ;
#33033=CARTESIAN_POINT ( 'NONE',  ( 989.9999999999992042, 56.73212367640085318, -362.5753187112032379 ) ) ;
#33034=ORIENTED_EDGE ( 'NONE', *, *, #17079, .F. ) ;
#33046=EDGE_LOOP ( 'NONE', ( #37130, #43304, #24433, #9144 ) ) ;
#33053=ORIENTED_EDGE ( 'NONE', *, *, #17095, .F. ) ;
#33082=EDGE_CURVE ( 'NONE', #23353, #20535, #38604, .T. ) ;
#33151=ORIENTED_EDGE ( 'NONE', *, *, #25839, .F. ) ;
#33217=EDGE_CURVE ( 'NONE', #10766, #11542, #2210, .T. ) ;
#33255=DIRECTION ( 'NONE',  ( 1.644774851296528363E-16, -1.000000000000000000, 0.000000000000000000 ) ) ;
#33303=EDGE_LOOP ( 'NONE', ( #27221, #26861, #44711, #10008 ) ) ;
#33311=EDGE_LOOP ( 'NONE', ( #14042, #40732, #1884, #15477 ) ) ;
#33345=EDGE_CURVE ( 'NONE', #20722, #6854, #16301, .T. ) ;
#33395=CARTESIAN_POINT ( 'NONE',  ( 999.9999999999992042, -590.0000000000001137, -350.0000000000000000 ) ) ;
#33404=ORIENTED_EDGE ( 'NONE', *, *, #22731, .T. ) ;
#33467=AXIS2_PLACEMENT_3D ( 'NONE', #28504, #42602, #10963 ) ;
#33473=DIRECTION ( 'NONE',  ( -1.000000000000000000, 0.000000000000000000, 0.000000000000000000 ) ) ;
#33475=DIRECTION ( 'NONE',  ( 1.000000000000000000, 0.000000000000000000, 0.000000000000000000 ) ) ;
#33476=CARTESIAN_POINT ( 'NONE',  ( 879.9999999999992042, 99.99999999999984368, 360.0000000000000000 ) ) ;
#33494=EDGE_CURVE ( 'NONE', #26364, #27491, #17456, .T. ) ;
#33495=DIRECTION ( 'NONE',  ( 0.000000000000000000, 1.000000000000000000, 0.000000000000000000 ) ) ;
#33545=LINE ( 'NONE', #12084, #22560 ) ;
#33586=CARTESIAN_POINT ( 'NONE',  ( 989.9999999999992042, 47.45399382421947365, 201.9999999999999432 ) ) ;
#33652=VECTOR ( 'NONE', #38874, 1000.000000000000114 ) ;
#33687=EDGE_CURVE ( 'NONE', #28026, #33818, #34303, .T. ) ;
#33725=VECTOR ( 'NONE', #30349, 1000.000000000000000 ) ;
#33726=ADVANCED_FACE ( 'NONE', ( #13529 ), #6460, .F. ) ;
#33749=ORIENTED_EDGE ( 'NONE', *, *, #37930, .F. ) ;
#33818=VERTEX_POINT ( 'NONE', #35444 ) ;
#33885=VERTEX_POINT ( 'NONE', #18141 ) ;
#33893=EDGE_LOOP ( 'NONE', ( #27448, #31027, #31699, #37155 ) ) ;
#33901=ORIENTED_EDGE ( 'NONE', *, *, #7216, .F. ) ;
#33911=CARTESIAN_POINT ( 'NONE',  ( 939.9999999999992042, 50.81038600091411439, 209.9999999999999716 ) ) ;
#33985=ORIENTED_EDGE ( 'NONE', *, *, #38013, .F. ) ;
#34060=CARTESIAN_POINT ( 'NONE',  ( 911.9999999999992042, 219.9999999999998863, -359.9749999999999659 ) ) ;
#34066=CARTESIAN_POINT ( 'NONE',  ( 927.9999999999993179, 154.9999999999998863, -359.9749999999999659 ) ) ;
#34208=EDGE_CURVE ( 'NONE', #43693, #1691, #12107, .T. ) ;
#34241=DIRECTION ( 'NONE',  ( 0.000000000000000000, 0.000000000000000000, 1.000000000000000000 ) ) ;
#34264=VECTOR ( 'NONE', #35037, 1000.000000000000000 ) ;
#34303=LINE ( 'NONE', #16993, #36689 ) ;
#34332=DIRECTION ( 'NONE',  ( -0.7071067811857625340, -8.659560562345319848E-17, -0.7071067811873326114 ) ) ;
#34339=ADVANCED_FACE ( 'NONE', ( #16244 ), #12769, .T. ) ;
#34376=VECTOR ( 'NONE', #45484, 1000.000000000000000 ) ;
#34404=VECTOR ( 'NONE', #28362, 999.9999999999998863 ) ;
#34410=CYLINDRICAL_SURFACE ( 'NONE', #22083, 1.000000000000000888 ) ;
#34453=EDGE_CURVE ( 'NONE', #3603, #29779, #21929, .T. ) ;
#34462=CARTESIAN_POINT ( 'NONE',  ( 989.9999999999992042, 249.9999999999998863, -360.0000000000000000 ) ) ;
#34465=CARTESIAN_POINT ( 'NONE',  ( 998.9999999999992042, -600.0000000000001137, -360.0000000000000000 ) ) ;
#34503=LINE ( 'NONE', #42115, #42750 ) ;
#34562=EDGE_CURVE ( 'NONE', #14035, #14977, #44889, .T. ) ;
#34577=ADVANCED_FACE ( 'NONE', ( #20836 ), #24073, .T. ) ;
#34584=FACE_OUTER_BOUND ( 'NONE', #14913, .T. ) ;
#34600=ORIENTED_EDGE ( 'NONE', *, *, #6377, .F. ) ;
#34661=DIRECTION ( 'NONE',  ( 0.000000000000000000, 0.000000000000000000, 1.000000000000000000 ) ) ;
#34734=DIRECTION ( 'NONE',  ( 0.000000000000000000, 0.000000000000000000, -1.000000000000000000 ) ) ;
#34737=CARTESIAN_POINT ( 'NONE',  ( 939.9999999999993179, -600.0000000000001137, -350.0000000000000000 ) ) ;
#34755=ORIENTED_EDGE ( 'NONE', *, *, #31758, .F. ) ;
#34759=DIRECTION ( 'NONE',  ( 1.000000000000000000, 0.000000000000000000, 0.000000000000000000 ) ) ;
#34769=ORIENTED_EDGE ( 'NONE', *, *, #26159, .T. ) ;
#34774=CARTESIAN_POINT ( 'NONE',  ( 927.9999999999990905, 154.9999999999998863, 360.0000000000000000 ) ) ;
#34798=DIRECTION ( 'NONE',  ( 1.000000000000000000, 0.000000000000000000, 0.000000000000000000 ) ) ;
#34831=CARTESIAN_POINT ( 'NONE',  ( 939.9999999999992042, -184.9457194955397767, -62.92409052808234549 ) ) ;
#34864=EDGE_CURVE ( 'NONE', #28618, #21201, #965, .T. ) ;
#34877=CARTESIAN_POINT ( 'NONE',  ( 914.9999999999992042, 99.99999999999984368, -360.0000000000000000 ) ) ;
#34910=CARTESIAN_POINT ( 'NONE',  ( 999.9999999999992042, 478.9999999999999432, 199.9999999999999716 ) ) ;
#34962=DIRECTION ( 'NONE',  ( 0.000000000000000000, 0.000000000000000000, -1.000000000000000000 ) ) ;
#34979=CARTESIAN_POINT ( 'NONE',  ( 879.9999999999992042, 99.99999999999984368, 360.0000000000000000 ) ) ;
#34983=VECTOR ( 'NONE', #8382, 1000.000000000000000 ) ;
#35005=DIRECTION ( 'NONE',  ( -0.000000000000000000, -0.000000000000000000, 1.000000000000000000 ) ) ;
#35037=DIRECTION ( 'NONE',  ( 0.000000000000000000, 0.000000000000000000, -1.000000000000000000 ) ) ;
#35042=PLANE ( 'NONE',  #37137 ) ;
#35066=VECTOR ( 'NONE', #3592, 1000.000000000000000 ) ;
#35069=DIRECTION ( 'NONE',  ( 0.000000000000000000, 0.7517448203044204691, -0.6594541114781790059 ) ) ;
#35072=VECTOR ( 'NONE', #43722, 1000.000000000000000 ) ;
#35085=DIRECTION ( 'NONE',  ( -0.000000000000000000, -0.000000000000000000, 1.000000000000000000 ) ) ;
#35110=ADVANCED_FACE ( 'NONE', ( #31917 ), #21990, .F. ) ;
#35121=LINE ( 'NONE', #39069, #1001 ) ;
#35138=LINE ( 'NONE', #7213, #21704 ) ;
#35198=VECTOR ( 'NONE', #32062, 1000.000000000000000 ) ;
#35200=LINE ( 'NONE', #34737, #8464 ) ;
#35203=DIRECTION ( 'NONE',  ( -1.058954862565134068E-16, 0.6438296778008191223, -0.7651688349527137056 ) ) ;
#35284=ORIENTED_EDGE ( 'NONE', *, *, #8056, .T. ) ;
#35302=CARTESIAN_POINT ( 'NONE',  ( 914.9999999999992042, 74.99999999999984368, -350.0000000000000000 ) ) ;
#35333=CARTESIAN_POINT ( 'NONE',  ( 939.9999999999992042, 56.73212367640090292, -362.5753187112032947 ) ) ;
#35413=CARTESIAN_POINT ( 'NONE',  ( 911.9999999999993179, 154.9999999999998863, -360.0000000000000000 ) ) ;
#35416=LINE ( 'NONE', #16740, #7558 ) ;
#35440=ADVANCED_FACE ( 'NONE', ( #41589 ), #2551, .T. ) ;
#35444=CARTESIAN_POINT ( 'NONE',  ( 999.9999999999992042, 248.9999999999998863, -359.0000000000000000 ) ) ;
#35496=DIRECTION ( 'NONE',  ( 0.000000000000000000, 0.000000000000000000, -1.000000000000000000 ) ) ;
#35519=CARTESIAN_POINT ( 'NONE',  ( 187.1337867209877857, 62.79977829742938411, 207.3621835540872951 ) ) ;
#35540=DIRECTION ( 'NONE',  ( -0.000000000000000000, -1.000000000000000000, -0.000000000000000000 ) ) ;
#35600=( BOUNDED_CURVE ( )  B_SPLINE_CURVE ( 3, ( #30828, #44921, #24108, #27356 ),
 .UNSPECIFIED., .F., .T. ) 
 B_SPLINE_CURVE_WITH_KNOTS ( ( 4, 4 ),
 ( 0.000000000000000000, 1.570796326794896558 ),
 .UNSPECIFIED. ) 
 CURVE ( )  GEOMETRIC_REPRESENTATION_ITEM ( )  RATIONAL_B_SPLINE_CURVE ( ( 1.000000000000000000, 0.8047378541243649375, 0.8047378541243649375, 1.000000000000000000 ) ) 
 REPRESENTATION_ITEM ( '' )  );
#35615=VERTEX_POINT ( 'NONE', #34877 ) ;
#35616=( NAMED_UNIT ( * ) SI_UNIT ( $, .STERADIAN. ) SOLID_ANGLE_UNIT ( ) );
#35629=EDGE_CURVE ( 'NONE', #19659, #12114, #38136, .T. ) ;
#35630=ORIENTED_EDGE ( 'NONE', *, *, #45636, .F. ) ;
#35649=VECTOR ( 'NONE', #28614, 1000.000000000000000 ) ;
#35689=EDGE_CURVE ( 'NONE', #21525, #8915, #45066, .T. ) ;
#35699=DIRECTION ( 'NONE',  ( 0.000000000000000000, 0.7651688349527167032, 0.6438296778008156807 ) ) ;
#35702=CARTESIAN_POINT ( 'NONE',  ( 939.9999999999993179, -190.2822455671962985, -69.00746428064724114 ) ) ;
#35723=CARTESIAN_POINT ( 'NONE',  ( 919.9999999999993179, 219.9999999999998863, -350.0000000000000000 ) ) ;
#35748=EDGE_CURVE ( 'NONE', #19255, #28334, #42268, .T. ) ;
#35762=LINE ( 'NONE', #21670, #36414 ) ;
#35773=VECTOR ( 'NONE', #43947, 1000.000000000000000 ) ;
#35777=FACE_OUTER_BOUND ( 'NONE', #39710, .T. ) ;
#35792=ORIENTED_EDGE ( 'NONE', *, *, #34453, .F. ) ;
#35798=DIRECTION ( 'NONE',  ( 1.000000000000000000, 0.000000000000000000, 0.000000000000000000 ) ) ;
#35856=DIRECTION ( 'NONE',  ( 1.644774851296528363E-16, -1.000000000000000000, 0.000000000000000000 ) ) ;
#35877=DIRECTION ( 'NONE',  ( -1.000000000000000000, 0.000000000000000000, 0.000000000000000000 ) ) ;
#35878=LINE ( 'NONE', #5294, #6389 ) ;
#35896=DIRECTION ( 'NONE',  ( 1.000000000000000000, 0.000000000000000000, 0.000000000000000000 ) ) ;
#35928=LINE ( 'NONE', #4298, #45462 ) ;
#35948=DIRECTION ( 'NONE',  ( 1.000000000000000000, 0.000000000000000000, 0.000000000000000000 ) ) ;
#35962=ORIENTED_EDGE ( 'NONE', *, *, #22429, .T. ) ;
#35964=EDGE_CURVE ( 'NONE', #16303, #10930, #24706, .T. ) ;
#35972=EDGE_CURVE ( 'NONE', #21525, #42633, #7872, .T. ) ;
#36030=ADVANCED_FACE ( 'NONE', ( #14796 ), #3482, .F. ) ;
#36036=ORIENTED_EDGE ( 'NONE', *, *, #31506, .T. ) ;
#36068=ADVANCED_FACE ( 'NONE', ( #34584 ), #3162, .T. ) ;
#36069=DIRECTION ( 'NONE',  ( 1.000000000000000000, 0.000000000000000000, -0.000000000000000000 ) ) ;
#36083=EDGE_CURVE ( 'NONE', #12726, #43693, #41514, .T. ) ;
#36106=DIRECTION ( 'NONE',  ( 1.000000000000000000, 0.000000000000000000, 0.000000000000000000 ) ) ;
#36114=FACE_OUTER_BOUND ( 'NONE', #5513, .T. ) ;
#36146=EDGE_LOOP ( 'NONE', ( #20061, #21224, #33901, #14411 ) ) ;
#36178=DIRECTION ( 'NONE',  ( 1.000000000000000000, 0.000000000000000000, 0.000000000000000000 ) ) ;
#36226=EDGE_CURVE ( 'NONE', #45131, #27073, #19773, .T. ) ;
#36239=LINE ( 'NONE', #33027, #33652 ) ;
#36243=EDGE_CURVE ( 'NONE', #577, #43693, #42197, .T. ) ;
#36271=ORIENTED_EDGE ( 'NONE', *, *, #14169, .F. ) ;
#36321=LINE ( 'NONE', #544, #10851 ) ;
#36354=ORIENTED_EDGE ( 'NONE', *, *, #11174, .T. ) ;
#36373=CARTESIAN_POINT ( 'NONE',  ( 999.9999999999992042, 249.5857864376267798, -359.5857864376268935 ) ) ;
#36375=ORIENTED_EDGE ( 'NONE', *, *, #32907, .F. ) ;
#36391=PLANE ( 'NONE',  #39396 ) ;
#36407=APPLICATION_CONTEXT ( 'automotive_design' ) ;
#36414=VECTOR ( 'NONE', #31382, 1000.000000000000000 ) ;
#36421=ORIENTED_EDGE ( 'NONE', *, *, #20102, .T. ) ;
#36439=CARTESIAN_POINT ( 'NONE',  ( 989.9999999999992042, -179.7356316342496712, -69.11609595480017276 ) ) ;
#36456=VERTEX_POINT ( 'NONE', #7787 ) ;
#36485=ORIENTED_EDGE ( 'NONE', *, *, #184, .T. ) ;
#36494=ORIENTED_EDGE ( 'NONE', *, *, #26116, .T. ) ;
#36522=AXIS2_PLACEMENT_3D ( 'NONE', #9600, #6363, #37772 ) ;
#36550=CIRCLE ( 'NONE', #42445, 7.999999999999785061 ) ;
#36585=DIRECTION ( 'NONE',  ( 1.644774851296528363E-16, -1.000000000000000000, 0.000000000000000000 ) ) ;
#36588=CIRCLE ( 'NONE', #10779, 8.024999999999948841 ) ;
#36614=ORIENTED_EDGE ( 'NONE', *, *, #40526, .T. ) ;
#36645=DIRECTION ( 'NONE',  ( 1.000000000000000000, 0.000000000000000000, 0.000000000000000000 ) ) ;
#36653=VECTOR ( 'NONE', #35877, 1000.000000000000000 ) ;
#36682=CARTESIAN_POINT ( 'NONE',  ( 939.9999999999992042, 74.99999999999984368, -360.0000000000000000 ) ) ;
#36689=VECTOR ( 'NONE', #45640, 1000.000000000000000 ) ;
#36742=CARTESIAN_POINT ( 'NONE',  ( 879.9999999999992042, 99.99999999999984368, -360.0000000000000000 ) ) ;
#36812=DIRECTION ( 'NONE',  ( 1.000000000000000000, 0.000000000000000000, 0.000000000000000000 ) ) ;
#36821=EDGE_CURVE ( 'NONE', #19659, #28329, #15913, .T. ) ;
#36870=DIRECTION ( 'NONE',  ( -0.000000000000000000, -1.000000000000000000, -0.000000000000000000 ) ) ;
#36879=ORIENTED_EDGE ( 'NONE', *, *, #20712, .F. ) ;
#36892=LINE ( 'NONE', #5462, #12305 ) ;
#36896=CARTESIAN_POINT ( 'NONE',  ( 989.9999999999992042, -407.8586036264140375, 201.9999999999998863 ) ) ;
#36942=CARTESIAN_POINT ( 'NONE',  ( 187.1337867209877857, 56.73212367640085318, -362.5753187112032379 ) ) ;
#36959=LINE ( 'NONE', #19408, #11745 ) ;
#37020=ORIENTED_EDGE ( 'NONE', *, *, #10316, .F. ) ;
#37054=CARTESIAN_POINT ( 'NONE',  ( 989.9999999999992042, 249.9999999999998863, 209.9999999999999716 ) ) ;
#37055=CARTESIAN_POINT ( 'NONE',  ( 998.9999999999992042, 249.9999999999998863, 199.9999999999999716 ) ) ;
#37071=VECTOR ( 'NONE', #42596, 1000.000000000000000 ) ;
#37084=EDGE_CURVE ( 'NONE', #27336, #19541, #16691, .T. ) ;
#37124=AXIS2_PLACEMENT_3D ( 'NONE', #28664, #42966, #14812 ) ;
#37130=ORIENTED_EDGE ( 'NONE', *, *, #43119, .F. ) ;
#37137=AXIS2_PLACEMENT_3D ( 'NONE', #4551, #15414, #18202 ) ;
#37155=ORIENTED_EDGE ( 'NONE', *, *, #5195, .F. ) ;
#37202=ORIENTED_EDGE ( 'NONE', *, *, #24100, .F. ) ;
#37204=CIRCLE ( 'NONE', #43130, 24.99999999999991118 ) ;
#37212=ORIENTED_EDGE ( 'NONE', *, *, #43627, .F. ) ;
#37273=CARTESIAN_POINT ( 'NONE',  ( 998.9999999999992042, 249.9999999999998863, -360.0000000000000000 ) ) ;
#37308=DIRECTION ( 'NONE',  ( -0.000000000000000000, -0.000000000000000000, -1.000000000000000000 ) ) ;
#37345=VECTOR ( 'NONE', #10676, 1000.000000000000000 ) ;
#37387=ORIENTED_EDGE ( 'NONE', *, *, #43236, .T. ) ;
#37418=EDGE_CURVE ( 'NONE', #20722, #5854, #15290, .T. ) ;
#37445=VECTOR ( 'NONE', #35856, 1000.000000000000000 ) ;
#37493=DIRECTION ( 'NONE',  ( -1.000000000000000000, 0.000000000000000000, 0.000000000000000000 ) ) ;
#37530=LINE ( 'NONE', #42134, #25366 ) ;
#37536=CARTESIAN_POINT ( 'NONE',  ( 998.9999999999992042, 479.9999999999999432, 360.0000000000000000 ) ) ;
#37608=ORIENTED_EDGE ( 'NONE', *, *, #20712, .T. ) ;
#37685=ADVANCED_FACE ( 'NONE', ( #22644 ), #29589, .F. ) ;
#37723=EDGE_CURVE ( 'NONE', #3030, #9195, #43219, .T. ) ;
#37724=ORIENTED_EDGE ( 'NONE', *, *, #2411, .F. ) ;
#37736=CYLINDRICAL_SURFACE ( 'NONE', #29243, 7.999999999999896083 ) ;
#37770=( BOUNDED_CURVE ( )  B_SPLINE_CURVE ( 3, ( #45458, #41526, #24409, #9878 ),
 .UNSPECIFIED., .F., .T. ) 
 B_SPLINE_CURVE_WITH_KNOTS ( ( 4, 4 ),
 ( 0.000000000000000000, 1.570796326794896558 ),
 .UNSPECIFIED. ) 
 CURVE ( )  GEOMETRIC_REPRESENTATION_ITEM ( )  RATIONAL_B_SPLINE_CURVE ( ( 1.000000000000000000, 0.8047378541243649375, 0.8047378541243649375, 1.000000000000000000 ) ) 
 REPRESENTATION_ITEM ( '' )  );
#37772=DIRECTION ( 'NONE',  ( 0.000000000000000000, -0.6438296778008192334, 0.7651688349527138167 ) ) ;
#37817=CARTESIAN_POINT ( 'NONE',  ( 999.9999999999992042, -599.0000000000001137, -359.0000000000000000 ) ) ;
#37873=LINE ( 'NONE', #27704, #39468 ) ;
#37910=DIRECTION ( 'NONE',  ( -1.000000000000000000, -4.625929269271485914E-16, -0.000000000000000000 ) ) ;
#37930=EDGE_CURVE ( 'NONE', #27336, #26364, #22867, .T. ) ;
#37951=CARTESIAN_POINT ( 'NONE',  ( 879.9999999999990905, 479.9999999999998863, 210.0000000000000000 ) ) ;
#37973=PLANE ( 'NONE',  #26292 ) ;
#37984=DIRECTION ( 'NONE',  ( -1.337618101958019798E-16, 1.000000000000000000, 1.672022627447524747E-16 ) ) ;
#37996=ADVANCED_FACE ( 'NONE', ( #9480 ), #34410, .T. ) ;
#38013=EDGE_CURVE ( 'NONE', #3415, #6890, #36959, .T. ) ;
#38046=LINE ( 'NONE', #44976, #39291 ) ;
#38129=DIRECTION ( 'NONE',  ( 1.000000000000000000, 4.625929269271485914E-16, 0.000000000000000000 ) ) ;
#38136=LINE ( 'NONE', #23782, #30855 ) ;
#38157=FACE_OUTER_BOUND ( 'NONE', #27122, .T. ) ;
#38208=EDGE_LOOP ( 'NONE', ( #38655, #45589, #39840, #18888 ) ) ;
#38218=ADVANCED_FACE ( 'NONE', ( #20996 ), #13402, .T. ) ;
#38236=DIRECTION ( 'NONE',  ( 0.000000000000000000, 0.000000000000000000, -1.000000000000000000 ) ) ;
#38255=ORIENTED_EDGE ( 'NONE', *, *, #39421, .T. ) ;
#38266=ORIENTED_EDGE ( 'NONE', *, *, #8889, .T. ) ;
#38272=DIRECTION ( 'NONE',  ( -1.000000000000000000, -4.625929269271485914E-16, -0.000000000000000000 ) ) ;
#38286=DIRECTION ( 'NONE',  ( 0.000000000000000000, 0.000000000000000000, -1.000000000000000000 ) ) ;
#38339=LINE ( 'NONE', #16635, #6270 ) ;
#38409=VERTEX_POINT ( 'NONE', #42487 ) ;
#38411=CARTESIAN_POINT ( 'NONE',  ( 187.1337867209877857, 50.81038600091411439, 193.6948738798775764 ) ) ;
#38429=ORIENTED_EDGE ( 'NONE', *, *, #26611, .T. ) ;
#38470=AXIS2_PLACEMENT_3D ( 'NONE', #726, #14824, #42979 ) ;
#38478=DIRECTION ( 'NONE',  ( 1.000000000000000000, 0.000000000000000000, 0.000000000000000000 ) ) ;
#38513=FACE_BOUND ( 'NONE', #6529, .T. ) ;
#38523=VERTEX_POINT ( 'NONE', #16261 ) ;
#38534=CARTESIAN_POINT ( 'NONE',  ( 989.9999999999992042, -590.0000000000001137, 350.0000000000000000 ) ) ;
#38555=VECTOR ( 'NONE', #32533, 999.9999999999998863 ) ;
#38562=DIRECTION ( 'NONE',  ( 0.000000000000000000, 0.000000000000000000, -1.000000000000000000 ) ) ;
#38604=CIRCLE ( 'NONE', #8375, 7.999999999999785061 ) ;
#38655=ORIENTED_EDGE ( 'NONE', *, *, #8842, .F. ) ;
#38743=CARTESIAN_POINT ( 'NONE',  ( 989.9999999999992042, -590.0000000000001137, -360.0000000000000000 ) ) ;
#38791=ORIENTED_EDGE ( 'NONE', *, *, #14169, .T. ) ;
#38807=CARTESIAN_POINT ( 'NONE',  ( 989.9999999999992042, 249.9999999999998863, -360.0000000000000000 ) ) ;
#38860=DIRECTION ( 'NONE',  ( 1.000000000000000000, 4.625929269271485914E-16, 0.000000000000000000 ) ) ;
#38874=DIRECTION ( 'NONE',  ( -0.000000000000000000, -0.6438296778008192334, 0.7651688349527135946 ) ) ;
#38934=DIRECTION ( 'NONE',  ( -1.000000000000000000, 2.412474565481389965E-32, 2.750100768424434704E-32 ) ) ;
#39019=PLANE ( 'NONE',  #31510 ) ;
#39058=EDGE_CURVE ( 'NONE', #20274, #3603, #34503, .T. ) ;
#39069=CARTESIAN_POINT ( 'NONE',  ( 998.9999999999992042, 479.9999999999999432, 360.0000000000000000 ) ) ;
#39125=CARTESIAN_POINT ( 'NONE',  ( 989.9999999999992042, -434.4637272565419153, -347.3621835540870393 ) ) ;
#39188=DIRECTION ( 'NONE',  ( 0.000000000000000000, 0.000000000000000000, -1.000000000000000000 ) ) ;
#39204=DIRECTION ( 'NONE',  ( 0.000000000000000000, 0.000000000000000000, -1.000000000000000000 ) ) ;
#39213=CIRCLE ( 'NONE', #19273, 7.999999999999896083 ) ;
#39218=ORIENTED_EDGE ( 'NONE', *, *, #6355, .T. ) ;
#39235=CARTESIAN_POINT ( 'NONE',  ( 919.9999999999993179, 154.9999999999998863, -360.0000000000000000 ) ) ;
#39238=DIRECTION ( 'NONE',  ( 1.000000000000000000, 0.000000000000000000, 0.000000000000000000 ) ) ;
#39291=VECTOR ( 'NONE', #19563, 1000.000000000000000 ) ;
#39297=FACE_OUTER_BOUND ( 'NONE', #12057, .T. ) ;
#39302=CARTESIAN_POINT ( 'NONE',  ( 187.1337867209877857, 62.85347435602256638, -357.4246812887967053 ) ) ;
#39309=EDGE_CURVE ( 'NONE', #41960, #19541, #42803, .T. ) ;
#39320=ORIENTED_EDGE ( 'NONE', *, *, #15003, .F. ) ;
#39340=ORIENTED_EDGE ( 'NONE', *, *, #36226, .F. ) ;
#39346=EDGE_LOOP ( 'NONE', ( #13525, #6366, #17323, #2283 ) ) ;
#39348=LINE ( 'NONE', #21782, #36653 ) ;
#39349=PLANE ( 'NONE',  #16706 ) ;
#39390=EDGE_CURVE ( 'NONE', #17002, #8608, #22013, .T. ) ;
#39395=VERTEX_POINT ( 'NONE', #39125 ) ;
#39396=AXIS2_PLACEMENT_3D ( 'NONE', #42655, #43100, #15392 ) ;
#39421=EDGE_CURVE ( 'NONE', #6074, #3415, #36321, .T. ) ;
#39424=DIRECTION ( 'NONE',  ( 0.000000000000000000, 0.000000000000000000, -1.000000000000000000 ) ) ;
#39457=EDGE_LOOP ( 'NONE', ( #36494, #44371, #9908, #43280 ) ) ;
#39468=VECTOR ( 'NONE', #41808, 1000.000000000000000 ) ;
#39469=CYLINDRICAL_SURFACE ( 'NONE', #4827, 7.999999999999896083 ) ;
#39477=DIRECTION ( 'NONE',  ( 1.000000000000000000, 0.000000000000000000, 0.000000000000000000 ) ) ;
#39493=DIRECTION ( 'NONE',  ( 1.000000000000000000, 0.000000000000000000, 0.000000000000000000 ) ) ;
#39497=DIRECTION ( 'NONE',  ( -1.000000000000000000, -4.625929269271485914E-16, -0.000000000000000000 ) ) ;
#39551=DIRECTION ( 'NONE',  ( 0.000000000000000000, -0.7651688349527138167, -0.6438296778008192334 ) ) ;
#39574=EDGE_LOOP ( 'NONE', ( #37202, #6424, #32922, #19131 ) ) ;
#39591=VECTOR ( 'NONE', #44798, 1000.000000000000000 ) ;
#39610=AXIS2_PLACEMENT_3D ( 'NONE', #8558, #19172, #29785 ) ;
#39649=DIRECTION ( 'NONE',  ( 1.000000000000000000, 4.625929269271485914E-16, 0.000000000000000000 ) ) ;
#39671=CARTESIAN_POINT ( 'NONE',  ( 506.1531787467675940, 50.81038600091411439, 217.3872392842761769 ) ) ;
#39710=EDGE_LOOP ( 'NONE', ( #38266, #12102, #10001, #44092 ) ) ;
#39716=LINE ( 'NONE', #15876, #38555 ) ;
#39733=DIRECTION ( 'NONE',  ( -4.625929269271485914E-16, 1.000000000000000000, 0.000000000000000000 ) ) ;
#39763=LINE ( 'NONE', #7886, #23325 ) ;
#39780=DIRECTION ( 'NONE',  ( 0.000000000000000000, -0.6438296778008192334, 0.7651688349527138167 ) ) ;
#39783=CARTESIAN_POINT ( 'NONE',  ( 914.9999999999992042, 46.15097736693707020, -350.0000000000000000 ) ) ;
#39840=ORIENTED_EDGE ( 'NONE', *, *, #3597, .T. ) ;
#39884=PLANE ( 'NONE',  #40107 ) ;
#39913=ORIENTED_EDGE ( 'NONE', *, *, #43236, .F. ) ;
#40025=DIRECTION ( 'NONE',  ( 4.625929269271485914E-16, -1.000000000000000000, 0.000000000000000000 ) ) ;
#40028=LINE ( 'NONE', #18342, #34983 ) ;
#40056=CARTESIAN_POINT ( 'NONE',  ( 919.9999999999993179, 219.9999999999998863, 350.0000000000000000 ) ) ;
#40064=ORIENTED_EDGE ( 'NONE', *, *, #30300, .F. ) ;
#40072=DIRECTION ( 'NONE',  ( 0.000000000000000000, 0.000000000000000000, 1.000000000000000000 ) ) ;
#40073=EDGE_LOOP ( 'NONE', ( #4254, #30736, #31968, #31768 ) ) ;
#40107=AXIS2_PLACEMENT_3D ( 'NONE', #3852, #25550, #32012 ) ;
#40110=DIRECTION ( 'NONE',  ( -0.000000000000000000, -0.000000000000000000, 1.000000000000000000 ) ) ;
#40113=ORIENTED_EDGE ( 'NONE', *, *, #41357, .F. ) ;
#40214=DIRECTION ( 'NONE',  ( -1.084653538143406060E-16, 0.6594541114781790059, 0.7517448203044204691 ) ) ;
#40236=VECTOR ( 'NONE', #8645, 1000.000000000000000 ) ;
#40269=VECTOR ( 'NONE', #30313, 1000.000000000000000 ) ;
#40353=ORIENTED_EDGE ( 'NONE', *, *, #8889, .F. ) ;
#40375=CARTESIAN_POINT ( 'NONE',  ( 939.9999999999992042, 56.73212367640090292, -362.5753187112032947 ) ) ;
#40428=DIRECTION ( 'NONE',  ( -1.236450975029139710E-16, 0.7517448203044212462, -0.6594541114781782287 ) ) ;
#40454=VECTOR ( 'NONE', #4177, 1000.000000000000114 ) ;
#40480=DIRECTION ( 'NONE',  ( 1.000000000000000000, 0.000000000000000000, 0.000000000000000000 ) ) ;
#40489=CARTESIAN_POINT ( 'NONE',  ( 919.9999999999993179, 154.9999999999998863, -350.0000000000000000 ) ) ;
#40492=DIRECTION ( 'NONE',  ( -1.000000000000000000, 0.000000000000000000, 0.000000000000000000 ) ) ;
#40501=ADVANCED_FACE ( 'NONE', ( #25175 ), #21033, .T. ) ;
#40523=ORIENTED_EDGE ( 'NONE', *, *, #184, .F. ) ;
#40526=EDGE_CURVE ( 'NONE', #10930, #20722, #35121, .T. ) ;
#40565=CARTESIAN_POINT ( 'NONE',  ( 919.9999999999993179, 154.9999999999998863, -360.0000000000000000 ) ) ;
#40567=EDGE_LOOP ( 'NONE', ( #6723, #33151, #41088, #27969 ) ) ;
#40582=ORIENTED_EDGE ( 'NONE', *, *, #2366, .F. ) ;
#40625=CARTESIAN_POINT ( 'NONE',  ( 911.9749999999993406, 154.9999999999998863, -360.0000000000000000 ) ) ;
#40626=VERTEX_POINT ( 'NONE', #33476 ) ;
#40637=ORIENTED_EDGE ( 'NONE', *, *, #22659, .F. ) ;
#40732=ORIENTED_EDGE ( 'NONE', *, *, #33345, .T. ) ;
#40753=LINE ( 'NONE', #37054, #10472 ) ;
#40759=CARTESIAN_POINT ( 'NONE',  ( 939.9999999999994316, -434.4637272565419153, -347.3621835540871530 ) ) ;
#40843=VECTOR ( 'NONE', #2870, 1000.000000000000000 ) ;
#40912=EDGE_LOOP ( 'NONE', ( #40353, #39913 ) ) ;
#40916=ADVANCED_FACE ( 'NONE', ( #19389 ), #22849, .T. ) ;
#41088=ORIENTED_EDGE ( 'NONE', *, *, #35748, .T. ) ;
#41113=AXIS2_PLACEMENT_3D ( 'NONE', #5853, #23392, #37493 ) ;
#41165=CARTESIAN_POINT ( 'NONE',  ( 989.9999999999992042, -190.2822455671962416, -69.00746428064729798 ) ) ;
#41204=ORIENTED_EDGE ( 'NONE', *, *, #28363, .T. ) ;
#41213=EDGE_LOOP ( 'NONE', ( #10638, #41591, #3711, #28833 ) ) ;
#41224=LINE ( 'NONE', #13276, #27501 ) ;
#41266=CARTESIAN_POINT ( 'NONE',  ( 914.9999999999992042, 99.99999999999984368, -360.0000000000000000 ) ) ;
#41279=CARTESIAN_POINT ( 'NONE',  ( 939.9999999999993179, 50.81038600091411439, 193.6948738798775764 ) ) ;
#41314=ORIENTED_EDGE ( 'NONE', *, *, #7816, .F. ) ;
#41342=EDGE_CURVE ( 'NONE', #38409, #29779, #17540, .T. ) ;
#41357=EDGE_CURVE ( 'NONE', #38523, #27925, #35762, .T. ) ;
#41371=ORIENTED_EDGE ( 'NONE', *, *, #31758, .T. ) ;
#41383=EDGE_CURVE ( 'NONE', #15632, #39395, #45717, .T. ) ;
#41386=ADVANCED_FACE ( 'NONE', ( #27922, #32309, #7370 ), #32063, .F. ) ;
#41401=CARTESIAN_POINT ( 'NONE',  ( 879.9999999999992042, 239.9999999999998010, -360.0000000000000000 ) ) ;
#41420=DIRECTION ( 'NONE',  ( -1.000000000000000000, 0.000000000000000000, 0.000000000000000000 ) ) ;
#41466=FACE_OUTER_BOUND ( 'NONE', #42721, .T. ) ;
#41484=ORIENTED_EDGE ( 'NONE', *, *, #6577, .T. ) ;
#41497=EDGE_CURVE ( 'NONE', #12114, #29177, #28366, .T. ) ;
#41514=LINE ( 'NONE', #38743, #13881 ) ;
#41526=CARTESIAN_POINT ( 'NONE',  ( 999.5857864376259840, 479.9999999999999432, 199.9999999999999432 ) ) ;
#41567=CARTESIAN_POINT ( 'NONE',  ( 919.9999999999993179, 219.9999999999998863, -360.0000000000000000 ) ) ;
#41580=LINE ( 'NONE', #16879, #32860 ) ;
#41589=FACE_OUTER_BOUND ( 'NONE', #25996, .T. ) ;
#41591=ORIENTED_EDGE ( 'NONE', *, *, #3268, .F. ) ;
#41620=DIRECTION ( 'NONE',  ( 0.000000000000000000, 0.000000000000000000, -1.000000000000000000 ) ) ;
#41657=ORIENTED_EDGE ( 'NONE', *, *, #28639, .F. ) ;
#41763=ORIENTED_EDGE ( 'NONE', *, *, #15648, .F. ) ;
#41776=CONICAL_SURFACE ( 'NONE', #43966, 8.024999999999948841, 0.7853981633963380560 ) ;
#41808=DIRECTION ( 'NONE',  ( 0.000000000000000000, 0.000000000000000000, -1.000000000000000000 ) ) ;
#41844=AXIS2_PLACEMENT_3D ( 'NONE', #15154, #1048, #10772 ) ;
#41883=VERTEX_POINT ( 'NONE', #11751 ) ;
#41885=EDGE_CURVE ( 'NONE', #15194, #45131, #39716, .T. ) ;
#41889=VERTEX_POINT ( 'NONE', #36896 ) ;
#41891=EDGE_LOOP ( 'NONE', ( #3077, #35630 ) ) ;
#41912=EDGE_CURVE ( 'NONE', #27925, #13298, #15445, .T. ) ;
#41926=DIRECTION ( 'NONE',  ( 0.000000000000000000, 0.000000000000000000, 1.000000000000000000 ) ) ;
#41960=VERTEX_POINT ( 'NONE', #8947 ) ;
#41983=DIRECTION ( 'NONE',  ( 1.000000000000000000, 0.000000000000000000, 0.000000000000000000 ) ) ;
#41989=CARTESIAN_POINT ( 'NONE',  ( 927.9999999999992042, 219.9999999999998863, 350.0000000000000000 ) ) ;
#41993=FACE_OUTER_BOUND ( 'NONE', #44021, .T. ) ;
#42094=ORIENTED_EDGE ( 'NONE', *, *, #2411, .T. ) ;
#42115=CARTESIAN_POINT ( 'NONE',  ( 911.9999999999993179, 219.9999999999998863, -360.0000000000000000 ) ) ;
#42119=LINE ( 'NONE', #9791, #17473 ) ;
#42123=DIRECTION ( 'NONE',  ( -1.644774851296528363E-16, 1.000000000000000000, 0.000000000000000000 ) ) ;
#42134=CARTESIAN_POINT ( 'NONE',  ( 939.9999999999992042, 62.85347435602262323, -357.4246812887967621 ) ) ;
#42160=EDGE_CURVE ( 'NONE', #43869, #31480, #38046, .T. ) ;
#42164=ORIENTED_EDGE ( 'NONE', *, *, #33494, .T. ) ;
#42174=VERTEX_POINT ( 'NONE', #16801 ) ;
#42185=CARTESIAN_POINT ( 'NONE',  ( 989.9999999999992042, 249.9999999999998863, -350.0000000000000000 ) ) ;
#42197=LINE ( 'NONE', #16581, #43390 ) ;
#42215=EDGE_CURVE ( 'NONE', #20750, #27073, #2933, .T. ) ;
#42237=CARTESIAN_POINT ( 'NONE',  ( 999.9999999999992042, 249.9999999999998863, 359.0000000000000000 ) ) ;
#42250=DIRECTION ( 'NONE',  ( 1.000000000000000000, 0.000000000000000000, 0.000000000000000000 ) ) ;
#42268=LINE ( 'NONE', #10872, #16111 ) ;
#42325=ORIENTED_EDGE ( 'NONE', *, *, #8056, .F. ) ;
#42363=CIRCLE ( 'NONE', #21720, 8.000000000000007105 ) ;
#42379=ORIENTED_EDGE ( 'NONE', *, *, #2366, .T. ) ;
#42396=VECTOR ( 'NONE', #26679, 1000.000000000000000 ) ;
#42415=AXIS2_PLACEMENT_3D ( 'NONE', #39302, #25667, #39780 ) ;
#42431=EDGE_CURVE ( 'NONE', #43930, #14210, #9407, .T. ) ;
#42445=AXIS2_PLACEMENT_3D ( 'NONE', #30868, #35005, #38478 ) ;
#42475=CARTESIAN_POINT ( 'NONE',  ( 879.9999999999990905, 469.9999999999998863, 210.0000000000000000 ) ) ;
#42479=EDGE_CURVE ( 'NONE', #5495, #9195, #11234, .T. ) ;
#42482=DIRECTION ( 'NONE',  ( 0.000000000000000000, 0.000000000000000000, -1.000000000000000000 ) ) ;
#42487=CARTESIAN_POINT ( 'NONE',  ( 927.9999999999990905, 219.9999999999998863, 360.0000000000000000 ) ) ;
#42521=AXIS2_PLACEMENT_3D ( 'NONE', #24790, #548, #28491 ) ;
#42540=CARTESIAN_POINT ( 'NONE',  ( 919.9999999999993179, 154.9999999999998863, -360.0000000000000000 ) ) ;
#42549=DIRECTION ( 'NONE',  ( 1.644774851296528363E-16, -1.000000000000000000, 0.000000000000000000 ) ) ;
#42565=AXIS2_PLACEMENT_3D ( 'NONE', #35519, #44852, #16674 ) ;
#42589=FACE_BOUND ( 'NONE', #41891, .T. ) ;
#42596=DIRECTION ( 'NONE',  ( 0.000000000000000000, -1.000000000000000000, 0.000000000000000000 ) ) ;
#42602=DIRECTION ( 'NONE',  ( 0.000000000000000000, 1.000000000000000000, 0.000000000000000000 ) ) ;
#42633=VERTEX_POINT ( 'NONE', #35702 ) ;
#42655=CARTESIAN_POINT ( 'NONE',  ( 1820.038553321469863, 240.0000000000001990, 201.9999999999999716 ) ) ;
#42695=CARTESIAN_POINT ( 'NONE',  ( 187.1337867209877857, 62.79977829742938411, 207.3621835540872951 ) ) ;
#42721=EDGE_LOOP ( 'NONE', ( #27064, #10801, #4676, #12546 ) ) ;
#42727=DIRECTION ( 'NONE',  ( -0.000000000000000000, 1.000000000000000000, -0.000000000000000000 ) ) ;
#42737=ORIENTED_EDGE ( 'NONE', *, *, #8842, .T. ) ;
#42750=VECTOR ( 'NONE', #10465, 1000.000000000000000 ) ;
#42757=DIRECTION ( 'NONE',  ( 4.625929269271485914E-16, -1.000000000000000000, 0.000000000000000000 ) ) ;
#42783=DIRECTION ( 'NONE',  ( 0.000000000000000000, 0.000000000000000000, -1.000000000000000000 ) ) ;
#42803=LINE ( 'NONE', #7256, #21892 ) ;
#42817=CYLINDRICAL_SURFACE ( 'NONE', #19521, 7.999999999999896083 ) ;
#42841=ORIENTED_EDGE ( 'NONE', *, *, #5210, .T. ) ;
#42915=DIRECTION ( 'NONE',  ( -0.000000000000000000, -0.000000000000000000, 1.000000000000000000 ) ) ;
#42966=DIRECTION ( 'NONE',  ( 0.000000000000000000, -1.000000000000000000, 0.000000000000000000 ) ) ;
#42979=DIRECTION ( 'NONE',  ( 1.000000000000000000, 4.625929269271485914E-16, 0.000000000000000000 ) ) ;
#43035=CARTESIAN_POINT ( 'NONE',  ( 989.9999999999992042, -419.8175818341089780, 209.9999999999999716 ) ) ;
#43057=DIRECTION ( 'NONE',  ( -1.084653538143406060E-16, 0.6594541114781790059, 0.7517448203044204691 ) ) ;
#43100=DIRECTION ( 'NONE',  ( -2.750100768424433062E-32, 1.672022627447525240E-16, -1.000000000000000000 ) ) ;
#43112=AXIS2_PLACEMENT_3D ( 'NONE', #9556, #26418, #1688 ) ;
#43113=AXIS2_PLACEMENT_3D ( 'NONE', #34462, #20593, #41620 ) ;
#43119=EDGE_CURVE ( 'NONE', #28026, #16303, #17412, .T. ) ;
#43125=ORIENTED_EDGE ( 'NONE', *, *, #16471, .F. ) ;
#43130=AXIS2_PLACEMENT_3D ( 'NONE', #328, #7281, #35896 ) ;
#43153=LINE ( 'NONE', #14534, #15981 ) ;
#43215=PLANE ( 'NONE',  #31364 ) ;
#43219=LINE ( 'NONE', #39783, #6581 ) ;
#43236=EDGE_CURVE ( 'NONE', #20274, #38409, #4661, .T. ) ;
#43240=ORIENTED_EDGE ( 'NONE', *, *, #5490, .F. ) ;
#43242=AXIS2_PLACEMENT_3D ( 'NONE', #43979, #26867, #12355 ) ;
#43255=CARTESIAN_POINT ( 'NONE',  ( 999.9999999999992042, -599.0000000000001137, 359.0000000000000000 ) ) ;
#43280=ORIENTED_EDGE ( 'NONE', *, *, #2421, .F. ) ;
#43304=ORIENTED_EDGE ( 'NONE', *, *, #33687, .T. ) ;
#43308=EDGE_CURVE ( 'NONE', #14977, #28819, #41224, .T. ) ;
#43315=EDGE_CURVE ( 'NONE', #4330, #12054, #44687, .T. ) ;
#43390=VECTOR ( 'NONE', #23936, 1000.000000000000000 ) ;
#43468=ORIENTED_EDGE ( 'NONE', *, *, #45636, .T. ) ;
#43480=ORIENTED_EDGE ( 'NONE', *, *, #14757, .F. ) ;
#43502=CARTESIAN_POINT ( 'NONE',  ( 919.9999999999993179, 219.9999999999998863, 350.0000000000000000 ) ) ;
#43513=ADVANCED_FACE ( 'NONE', ( #19971 ), #15038, .F. ) ;
#43528=LINE ( 'NONE', #25966, #18170 ) ;
#43545=CARTESIAN_POINT ( 'NONE',  ( 928.0249999999991815, 219.9999999999998863, -360.0000000000000000 ) ) ;
#43592=DIRECTION ( 'NONE',  ( -0.000000000000000000, -0.000000000000000000, 1.000000000000000000 ) ) ;
#43595=CARTESIAN_POINT ( 'NONE',  ( 989.9999999999992042, 249.9999999999998863, 209.9999999999999716 ) ) ;
#43627=EDGE_CURVE ( 'NONE', #22885, #5495, #32592, .T. ) ;
#43640=EDGE_LOOP ( 'NONE', ( #38255, #6079, #19062, #12226, #42164, #2337, #16592 ) ) ;
#43691=AXIS2_PLACEMENT_3D ( 'NONE', #35302, #10833, #24669 ) ;
#43693=VERTEX_POINT ( 'NONE', #38534 ) ;
#43722=DIRECTION ( 'NONE',  ( 0.000000000000000000, 0.000000000000000000, 1.000000000000000000 ) ) ;
#43732=ORIENTED_EDGE ( 'NONE', *, *, #13049, .F. ) ;
#43767=CARTESIAN_POINT ( 'NONE',  ( 911.9999999999994316, 154.9999999999998863, 360.0000000000000000 ) ) ;
#43828=ORIENTED_EDGE ( 'NONE', *, *, #6400, .F. ) ;
#43835=ORIENTED_EDGE ( 'NONE', *, *, #11411, .F. ) ;
#43869=VERTEX_POINT ( 'NONE', #34831 ) ;
#43879=EDGE_CURVE ( 'NONE', #5823, #35615, #3671, .T. ) ;
#43902=AXIS2_PLACEMENT_3D ( 'NONE', #43502, #30312, #11869 ) ;
#43910=ORIENTED_EDGE ( 'NONE', *, *, #21483, .F. ) ;
#43919=ORIENTED_EDGE ( 'NONE', *, *, #42160, .T. ) ;
#43925=DIRECTION ( 'NONE',  ( -0.000000000000000000, -0.000000000000000000, 1.000000000000000000 ) ) ;
#43930=VERTEX_POINT ( 'NONE', #36682 ) ;
#43947=DIRECTION ( 'NONE',  ( 0.000000000000000000, 0.000000000000000000, -1.000000000000000000 ) ) ;
#43953=DIRECTION ( 'NONE',  ( 0.000000000000000000, 1.000000000000000000, 0.000000000000000000 ) ) ;
#43954=CARTESIAN_POINT ( 'NONE',  ( 879.9999999999990905, -419.8175818341089780, 210.0000000000000000 ) ) ;
#43956=VERTEX_POINT ( 'NONE', #23254 ) ;
#43957=VECTOR ( 'NONE', #2130, 1000.000000000000114 ) ;
#43966=AXIS2_PLACEMENT_3D ( 'NONE', #6428, #35496, #10803 ) ;
#43979=CARTESIAN_POINT ( 'NONE',  ( 914.9999999999992042, 74.99999999999984368, -360.0000000000000000 ) ) ;
#44021=EDGE_LOOP ( 'NONE', ( #32188, #21470, #41314, #6199 ) ) ;
#44034=CIRCLE ( 'NONE', #17518, 24.99999999999991118 ) ;
#44052=ORIENTED_EDGE ( 'NONE', *, *, #8646, .T. ) ;
#44068=DIRECTION ( 'NONE',  ( 1.644774851296528363E-16, -1.000000000000000000, 0.000000000000000000 ) ) ;
#44080=CARTESIAN_POINT ( 'NONE',  ( 939.9999999999992042, 74.99999999999984368, 360.0000000000000000 ) ) ;
#44092=ORIENTED_EDGE ( 'NONE', *, *, #41342, .F. ) ;
#44098=CARTESIAN_POINT ( 'NONE',  ( 1820.038553321469863, 240.0000000000001990, 201.9999999999999716 ) ) ;
#44117=CARTESIAN_POINT ( 'NONE',  ( 998.9999999999992042, 478.9999999999999432, 0.000000000000000000 ) ) ;
#44174=CARTESIAN_POINT ( 'NONE',  ( 939.9999999999993179, -418.3138125091625170, 201.9999999999998863 ) ) ;
#44181=LINE ( 'NONE', #4941, #45442 ) ;
#44243=EDGE_CURVE ( 'NONE', #35615, #43930, #242, .T. ) ;
#44289=FACE_OUTER_BOUND ( 'NONE', #19818, .T. ) ;
#44310=DIRECTION ( 'NONE',  ( 0.000000000000000000, -1.000000000000000000, 0.000000000000000000 ) ) ;
#44311=ORIENTED_EDGE ( 'NONE', *, *, #21483, .T. ) ;
#44363=ORIENTED_EDGE ( 'NONE', *, *, #13974, .T. ) ;
#44371=ORIENTED_EDGE ( 'NONE', *, *, #7195, .F. ) ;
#44400=DIRECTION ( 'NONE',  ( -0.000000000000000000, -0.000000000000000000, 1.000000000000000000 ) ) ;
#44409=ORIENTED_EDGE ( 'NONE', *, *, #14757, .T. ) ;
#44436=CARTESIAN_POINT ( 'NONE',  ( 919.9999999999993179, 154.9999999999998863, -360.0000000000000000 ) ) ;
#44541=LINE ( 'NONE', #33033, #6213 ) ;
#44558=CARTESIAN_POINT ( 'NONE',  ( 999.9999999999992042, 249.9999999999998863, -360.0000000000000000 ) ) ;
#44563=ORIENTED_EDGE ( 'NONE', *, *, #36243, .F. ) ;
#44671=ADVANCED_FACE ( 'NONE', ( #15165 ), #39884, .F. ) ;
#44682=FACE_OUTER_BOUND ( 'NONE', #21890, .T. ) ;
#44687=LINE ( 'NONE', #16741, #7606 ) ;
#44701=CONICAL_SURFACE ( 'NONE', #1914, 8.024999999999948841, 0.7853981633963380560 ) ;
#44702=LINE ( 'NONE', #3107, #14346 ) ;
#44711=ORIENTED_EDGE ( 'NONE', *, *, #6377, .T. ) ;
#44736=CARTESIAN_POINT ( 'NONE',  ( 989.9999999999992042, -416.7569064942979935, 212.5753187112032947 ) ) ;
#44738=ADVANCED_FACE ( 'NONE', ( #32485 ), #36391, .T. ) ;
#44772=VECTOR ( 'NONE', #39477, 1000.000000000000000 ) ;
#44796=EDGE_LOOP ( 'NONE', ( #17169, #44563, #7597, #36271, #21784, #40113, #8361 ) ) ;
#44798=DIRECTION ( 'NONE',  ( -0.000000000000000000, -1.000000000000000000, 0.000000000000000000 ) ) ;
#44821=DIRECTION ( 'NONE',  ( 0.000000000000000000, 0.000000000000000000, -1.000000000000000000 ) ) ;
#44852=DIRECTION ( 'NONE',  ( 0.000000000000000000, 0.7517448203044204691, -0.6594541114781790059 ) ) ;
#44889=LINE ( 'NONE', #38411, #17515 ) ;
#44913=CARTESIAN_POINT ( 'NONE',  ( 879.9999999999992042, 239.9999999999998295, -350.0000000000000000 ) ) ;
#44921=CARTESIAN_POINT ( 'NONE',  ( 999.5857864376259840, 479.9999999999999432, 360.0000000000000000 ) ) ;
#44924=DIRECTION ( 'NONE',  ( 0.000000000000000000, -0.6594541114781790059, -0.7517448203044204691 ) ) ;
#44931=DIRECTION ( 'NONE',  ( -1.000000000000000000, 0.000000000000000000, 0.000000000000000000 ) ) ;
#44941=ORIENTED_EDGE ( 'NONE', *, *, #43879, .T. ) ;
#44965=ADVANCED_FACE ( 'NONE', ( #11238 ), #14934, .F. ) ;
#44976=CARTESIAN_POINT ( 'NONE',  ( 187.1337867209877857, -184.9457194955397199, -62.92409052808242365 ) ) ;
#45066=LINE ( 'NONE', #10397, #25680 ) ;
#45120=ORIENTED_EDGE ( 'NONE', *, *, #30109, .F. ) ;
#45131=VERTEX_POINT ( 'NONE', #43545 ) ;
#45145=PLANE ( 'NONE',  #1806 ) ;
#45318=EDGE_CURVE ( 'NONE', #19255, #1155, #37530, .T. ) ;
#45365=CARTESIAN_POINT ( 'NONE',  ( 187.1337867209877857, 56.78581973499402835, 212.6378164459127049 ) ) ;
#45369=VECTOR ( 'NONE', #44068, 1000.000000000000000 ) ;
#45378=DIRECTION ( 'NONE',  ( -0.000000000000000000, -0.6438296778008192334, 0.7651688349527135946 ) ) ;
#45405=ORIENTED_EDGE ( 'NONE', *, *, #27310, .T. ) ;
#45442=VECTOR ( 'NONE', #26406, 1000.000000000000000 ) ;
#45446=DIRECTION ( 'NONE',  ( -0.000000000000000000, -0.000000000000000000, 1.000000000000000000 ) ) ;
#45458=CARTESIAN_POINT ( 'NONE',  ( 998.9999999999992042, 479.9999999999999432, 199.9999999999999716 ) ) ;
#45462=VECTOR ( 'NONE', #5394, 1000.000000000000000 ) ;
#45484=DIRECTION ( 'NONE',  ( -1.000000000000000000, -1.644774851296528363E-16, -0.000000000000000000 ) ) ;
#45486=LINE ( 'NONE', #17989, #35198 ) ;
#45544=ORIENTED_EDGE ( 'NONE', *, *, #37084, .T. ) ;
#45589=ORIENTED_EDGE ( 'NONE', *, *, #10862, .F. ) ;
#45636=EDGE_CURVE ( 'NONE', #20535, #23353, #9175, .T. ) ;
#45640=DIRECTION ( 'NONE',  ( -0.000000000000000000, -0.000000000000000000, -1.000000000000000000 ) ) ;
#45717=LINE ( 'NONE', #28142, #32666 ) ;
#45724=LINE ( 'NONE', #42475, #12320 ) ;
#45738=COLOUR_RGB('Dark Blue',0.08,0.2,0.34);
#45739=FILL_AREA_STYLE_COLOUR('',#45738);
#45740=FILL_AREA_STYLE('',(#45739));
#45741=SURFACE_STYLE_FILL_AREA(#45740);
#45742=SURFACE_SIDE_STYLE('',(#45741));
#45743=SURFACE_STYLE_USAGE(.BOTH.,#45742);
#45744=PRESENTATION_STYLE_ASSIGNMENT((#45743));
ENDSEC;
END-ISO-10303-21;
